ISO-10303-21;
HEADER;
FILE_DESCRIPTION (('STEP AP214'),
    '1' );
FILE_NAME ('Snap Open Cable Crossbars 2.step',
    '2026-10-08T22:59:04',
    ( '' ),
    ( '' ),
    'SwSTEP 2.0',
    'SolidWorks 2020',
    '' );
FILE_SCHEMA (( 'AUTOMOTIVE_DESIGN' ));
ENDSEC;

DATA;
#19=ORIENTED_EDGE ( 'NONE', *, *, #38836, .T. ) ;
#248=( NAMED_UNIT ( * ) SI_UNIT ( $, .STERADIAN. ) SOLID_ANGLE_UNIT ( ) );
#331=EDGE_CURVE ( 'NONE', #102761, #231063, #231938, .T. ) ;
#479=CARTESIAN_POINT ( 'NONE',  ( -17.11825945287481687, 9.950000000011138823, -54.25000000000000711 ) ) ;
#793=CARTESIAN_POINT ( 'NONE',  ( -16.80070461187922959, 9.950000000011137047, -46.14696382916198303 ) ) ;
#815=EDGE_CURVE ( 'NONE', #144454, #50955, #20274, .T. ) ;
#895=CARTESIAN_POINT ( 'NONE',  ( 18.54999999999999716, 9.950000000011153034, -46.14999999999994884 ) ) ;
#936=VERTEX_POINT ( 'NONE', #30232 ) ;
#1058=PLANE ( 'NONE',  #110612 ) ;
#1115=ADVANCED_FACE ( 'NONE', ( #182586 ), #85999, .T. ) ;
#1195=LINE ( 'NONE', #182443, #193762 ) ;
#1277=DIRECTION ( 'NONE',  ( 1.000000000000000000, 0.000000000000000000, 0.000000000000000000 ) ) ;
#1281=CARTESIAN_POINT ( 'NONE',  ( 16.87683809663749557, 9.950000000011131718, -54.35000000000000142 ) ) ;
#1320=CARTESIAN_POINT ( 'NONE',  ( 20.73486653747088226, 7.250000000011182166, -46.15000000000000568 ) ) ;
#1335=( BOUNDED_CURVE ( )  B_SPLINE_CURVE ( 3, ( #84635, #62558, #164232, #200777 ),
 .UNSPECIFIED., .F., .F. ) 
 B_SPLINE_CURVE_WITH_KNOTS ( ( 4, 4 ),
 ( 1.570796326794885012, 3.141592653589794448 ),
 .UNSPECIFIED. ) 
 CURVE ( )  GEOMETRIC_REPRESENTATION_ITEM ( )  RATIONAL_B_SPLINE_CURVE ( ( 1.000000000000000000, 0.8047378541243619399, 0.8047378541243619399, 1.000000000000000000 ) ) 
 REPRESENTATION_ITEM ( '' )  );
#1550=CARTESIAN_POINT ( 'NONE',  ( 22.88900146558018989, 8.703904791123973084, -46.15000000000001279 ) ) ;
#1575=CARTESIAN_POINT ( 'NONE',  ( -16.78270389226384296, 9.947372616628161524, -54.34120703691146304 ) ) ;
#1665=ORIENTED_EDGE ( 'NONE', *, *, #203874, .F. ) ;
#1780=ORIENTED_EDGE ( 'NONE', *, *, #72524, .T. ) ;
#1872=CARTESIAN_POINT ( 'NONE',  ( -21.64999999999999858, 10.05000000001113847, -54.25000000000000711 ) ) ;
#1951=ORIENTED_EDGE ( 'NONE', *, *, #237695, .T. ) ;
#2018=FACE_OUTER_BOUND ( 'NONE', #178784, .T. ) ;
#2041=CARTESIAN_POINT ( 'NONE',  ( -16.87372386987899020, 9.880600233647912845, -46.64926987186640162 ) ) ;
#2081=CARTESIAN_POINT ( 'NONE',  ( 15.74999999999999645, 9.850000000011137402, -50.24999999999999289 ) ) ;
#2207=CARTESIAN_POINT ( 'NONE',  ( -16.77977881697927032, 9.946601933544062746, -46.16137857311505854 ) ) ;
#2425=AXIS2_PLACEMENT_3D ( 'NONE', #153513, #135160, #16531 ) ;
#2531=EDGE_LOOP ( 'NONE', ( #116566, #111181, #239458, #229281, #15993, #112213, #10452, #49800, #222333, #180469 ) ) ;
#2724=CARTESIAN_POINT ( 'NONE',  ( -17.73285935861207818, 10.85798180380284528, -43.74143819021772828 ) ) ;
#2821=VERTEX_POINT ( 'NONE', #200302 ) ;
#2877=CARTESIAN_POINT ( 'NONE',  ( -18.34374000495060386, 11.47316190337362585, -42.74999999999999289 ) ) ;
#2908=CARTESIAN_POINT ( 'NONE',  ( -12.25000000000000178, 9.850000000011133849, -50.25000000000000711 ) ) ;
#3108=EDGE_LOOP ( 'NONE', ( #251915, #214247, #181986, #186028 ) ) ;
#3587=PLANE ( 'NONE',  #247838 ) ;
#3608=CARTESIAN_POINT ( 'NONE',  ( 12.25000000000000000, 9.350000000011140955, -50.24999999999999289 ) ) ;
#3728=EDGE_CURVE ( 'NONE', #151965, #936, #31045, .T. ) ;
#3851=PLANE ( 'NONE',  #205364 ) ;
#4232=ORIENTED_EDGE ( 'NONE', *, *, #44939, .T. ) ;
#4237=EDGE_CURVE ( 'NONE', #105073, #97258, #44028, .T. ) ;
#4243=CARTESIAN_POINT ( 'NONE',  ( -16.81744102076749314, 9.950000000011142376, -46.15000000000000568 ) ) ;
#4305=CARTESIAN_POINT ( 'NONE',  ( 20.73486653747088582, 7.250000000011182166, -54.35000000000000142 ) ) ;
#4324=FACE_OUTER_BOUND ( 'NONE', #130623, .T. ) ;
#4355=VECTOR ( 'NONE', #136966, 1000.000000000000000 ) ;
#4551=CARTESIAN_POINT ( 'NONE',  ( -13.77178122865954535, 9.456028260519072859, -48.51119803506571770 ) ) ;
#4763=CARTESIAN_POINT ( 'NONE',  ( -16.77683809663752257, 9.945835743215301505, -46.16394901910421567 ) ) ;
#4803=CYLINDRICAL_SURFACE ( 'NONE', #182232, 1.749999999999998002 ) ;
#4850=CARTESIAN_POINT ( 'NONE',  ( -16.87683809663752399, 21.23804903844422043, -46.15000000000000568 ) ) ;
#5214=ORIENTED_EDGE ( 'NONE', *, *, #219203, .F. ) ;
#5229=CYLINDRICAL_SURFACE ( 'NONE', #232941, 0.09999999999999939493 ) ;
#5289=ORIENTED_EDGE ( 'NONE', *, *, #192125, .T. ) ;
#5312=ORIENTED_EDGE ( 'NONE', *, *, #49985, .T. ) ;
#5330=AXIS2_PLACEMENT_3D ( 'NONE', #135100, #155992, #94700 ) ;
#5461=CARTESIAN_POINT ( 'NONE',  ( -15.55912972643740488, 8.490870273573721150, -54.45000000000000284 ) ) ;
#5609=FACE_OUTER_BOUND ( 'NONE', #173510, .T. ) ;
#5835=CARTESIAN_POINT ( 'NONE',  ( 12.25000000000000355, 9.350000000011142731, -50.02151937182512142 ) ) ;
#5903=CARTESIAN_POINT ( 'NONE',  ( -21.65000000000000213, 7.250000000011138646, -42.75000000000000000 ) ) ;
#5973=EDGE_CURVE ( 'NONE', #155471, #154908, #136935, .T. ) ;
#6375=EDGE_LOOP ( 'NONE', ( #175652, #142207, #234862, #192897, #188378 ) ) ;
#6377=ORIENTED_EDGE ( 'NONE', *, *, #192254, .F. ) ;
#6403=EDGE_CURVE ( 'NONE', #151965, #228728, #177252, .T. ) ;
#6559=AXIS2_PLACEMENT_3D ( 'NONE', #139775, #159376, #219324 ) ;
#6572=ORIENTED_EDGE ( 'NONE', *, *, #7037, .F. ) ;
#6612=ORIENTED_EDGE ( 'NONE', *, *, #198342, .T. ) ;
#6829=CARTESIAN_POINT ( 'NONE',  ( -16.92989143108097849, 9.950000000011137047, -46.38248387475668011 ) ) ;
#6920=CARTESIAN_POINT ( 'NONE',  ( -20.65000000000000568, 5.650000000011139001, -42.75000000000000000 ) ) ;
#6938=CARTESIAN_POINT ( 'NONE',  ( -16.97683810757273193, 9.950000000011137047, -53.73642328753960129 ) ) ;
#7037=EDGE_CURVE ( 'NONE', #22095, #91552, #248106, .T. ) ;
#7118=CARTESIAN_POINT ( 'NONE',  ( -15.52965525596987995, 9.375538102059161716, -49.36987588099083979 ) ) ;
#7130=CARTESIAN_POINT ( 'NONE',  ( 15.15590539855246810, 9.410682294279112625, -48.93114344194827936 ) ) ;
#7154=CIRCLE ( 'NONE', #44603, 1.749999999999999778 ) ;
#7170=CIRCLE ( 'NONE', #215474, 1.500000000000001332 ) ;
#7176=CARTESIAN_POINT ( 'NONE',  ( -16.83794237512073622, 9.926359221118632448, -46.30354215869895995 ) ) ;
#7445=LINE ( 'NONE', #126099, #93043 ) ;
#7657=AXIS2_PLACEMENT_3D ( 'NONE', #154165, #15926, #58841 ) ;
#7793=FACE_OUTER_BOUND ( 'NONE', #103774, .T. ) ;
#8071=CYLINDRICAL_SURFACE ( 'NONE', #58596, 0.1000000000000013656 ) ;
#8309=CARTESIAN_POINT ( 'NONE',  ( 13.88638282980484107, 9.457426452500056868, -52.00004186840002518 ) ) ;
#8426=LINE ( 'NONE', #161086, #59093 ) ;
#8437=CARTESIAN_POINT ( 'NONE',  ( 14.22821877134046531, 9.456028260519072859, -48.51119803506571060 ) ) ;
#8545=ORIENTED_EDGE ( 'NONE', *, *, #219137, .T. ) ;
#8585=FACE_OUTER_BOUND ( 'NONE', #255240, .T. ) ;
#8678=ORIENTED_EDGE ( 'NONE', *, *, #174264, .T. ) ;
#9137=CARTESIAN_POINT ( 'NONE',  ( -16.97048361161167662, 9.950000000011138823, -53.85888434443041461 ) ) ;
#9321=CARTESIAN_POINT ( 'NONE',  ( -17.78043020864320667, 10.85359211201683927, -43.83695083427979000 ) ) ;
#9504=CARTESIAN_POINT ( 'NONE',  ( -16.79270642812322123, 9.946244216949036598, -54.33893327856191746 ) ) ;
#9703=CARTESIAN_POINT ( 'NONE',  ( 14.56326696814971555, 9.446648990640015953, -48.58916329592317851 ) ) ;
#9728=VERTEX_POINT ( 'NONE', #83954 ) ;
#9776=( BOUNDED_SURFACE ( )  B_SPLINE_SURFACE ( 3, 2, ( 
 ( #19100, #37407, #179487 ),
 ( #98598, #114362, #238142 ),
 ( #116927, #17809, #157371 ),
 ( #257649, #137750, #58210 ),
 ( #97321, #213453, #195209 ),
 ( #178211, #218571, #38676 ),
 ( #176928, #118210, #236863 ),
 ( #77777, #39987, #96061 ),
 ( #174383, #793, #175635 ),
 ( #79050, #253850, #156088 ) ),
 .UNSPECIFIED., .F., .F., .F. ) 
 B_SPLINE_SURFACE_WITH_KNOTS ( ( 4, 2, 2, 2, 4 ),
 ( 3, 3 ),
 ( 0.002161241639767792072, 0.002579950749617451571, 0.002789305304542281753, 0.002893982582004696845, 0.002998659859467111503 ),
 ( 0.000000000000000000, 1.000000000000000000 ),
 .UNSPECIFIED. ) 
 GEOMETRIC_REPRESENTATION_ITEM ( )  RATIONAL_B_SPLINE_SURFACE ( (
 ( 1.000000000000000000, 0.7071067811864923947, 1.000000000000000000),
 ( 1.000000000000000000, 0.7632447400663602277, 1.000000000000000000),
 ( 1.000000000000000000, 0.8158073005109875986, 1.000000000000000000),
 ( 1.000000000000000000, 0.8906973462395570973, 1.000000000000000000),
 ( 1.000000000000000000, 0.9149408947799901881, 1.000000000000000000),
 ( 1.000000000000000000, 0.9493368785275747568, 1.000000000000000000),
 ( 1.000000000000000000, 0.9605194247156804144, 1.000000000000000000),
 ( 1.000000000000000000, 0.9803630264780990311, 1.000000000000000000),
 ( 1.000000000000000000, 0.9900844824271254341, 1.000000000000000000),
 ( 1.000000000000000000, 0.9894588281429296250, 1.000000000000000000) ) ) 
 REPRESENTATION_ITEM ( '' )  SURFACE ( )  );
#10198=VECTOR ( 'NONE', #164809, 1000.000000000000000 ) ;
#10452=ORIENTED_EDGE ( 'NONE', *, *, #172169, .F. ) ;
#10494=CARTESIAN_POINT ( 'NONE',  ( -16.87665923198281348, 9.950000000011138823, -54.35000000000000142 ) ) ;
#10496=CARTESIAN_POINT ( 'NONE',  ( -16.89318236219976299, 9.951535257886286345, -54.35512963210585724 ) ) ;
#10802=CARTESIAN_POINT ( 'NONE',  ( -16.87333278164147288, 9.882609784590036028, -53.86683219384699584 ) ) ;
#10873=CARTESIAN_POINT ( 'NONE',  ( 18.39999999999997371, 11.47316190337362940, -57.75000000000000711 ) ) ;
#11402=ORIENTED_EDGE ( 'NONE', *, *, #98664, .F. ) ;
#11507=ORIENTED_EDGE ( 'NONE', *, *, #29484, .F. ) ;
#11844=PRODUCT_CONTEXT ( 'NONE', #168951, 'mechanical' ) ;
#12004=AXIS2_PLACEMENT_3D ( 'NONE', #81226, #121683, #198623 ) ;
#12357=DIRECTION ( 'NONE',  ( 0.7071067811865463515, -0.7071067811865487940, 0.000000000000000000 ) ) ;
#12399=CARTESIAN_POINT ( 'NONE',  ( -16.87331047859651179, 9.950000000011142376, -46.15000000000000568 ) ) ;
#12441=ORIENTED_EDGE ( 'NONE', *, *, #127715, .F. ) ;
#12466=CIRCLE ( 'NONE', #145527, 0.9000000000000014655 ) ;
#12490=CARTESIAN_POINT ( 'NONE',  ( -16.94445028196808778, 9.992063609708889516, -46.10733017841845793 ) ) ;
#12528=DIRECTION ( 'NONE',  ( 0.000000000000000000, 1.000000000000000000, 0.000000000000000000 ) ) ;
#12613=CARTESIAN_POINT ( 'NONE',  ( -16.27683809663750480, 9.350000000011133849, -54.44999999999999574 ) ) ;
#12787=DIRECTION ( 'NONE',  ( 0.000000000000000000, 0.000000000000000000, -1.000000000000000000 ) ) ;
#12965=CARTESIAN_POINT ( 'NONE',  ( 21.72449340488910252, 10.28395627750227703, -46.15000000000001279 ) ) ;
#13021=CARTESIAN_POINT ( 'NONE',  ( -18.39999999999999858, 11.47316190337362585, -42.79982924846601122 ) ) ;
#13076=CARTESIAN_POINT ( 'NONE',  ( -16.94878442675511820, 9.991729103002159107, -54.38821957563787635 ) ) ;
#13145=ORIENTED_EDGE ( 'NONE', *, *, #94052, .F. ) ;
#13425=CARTESIAN_POINT ( 'NONE',  ( 20.73486653747088582, 7.250000000011182166, -46.15000000000000568 ) ) ;
#13438=CARTESIAN_POINT ( 'NONE',  ( 12.60873083341396494, 9.389571634557560387, -51.31764071236915470 ) ) ;
#13635=CIRCLE ( 'NONE', #155319, 0.5000000000000004441 ) ;
#13652=CARTESIAN_POINT ( 'NONE',  ( -18.40000000000000213, 8.822561741677553471, -57.75000000000000000 ) ) ;
#13855=ORIENTED_EDGE ( 'NONE', *, *, #119576, .T. ) ;
#13876=DIRECTION ( 'NONE',  ( 0.000000000000000000, -1.000000000000000000, 0.000000000000000000 ) ) ;
#13920=LINE ( 'NONE', #94720, #159953 ) ;
#13921=CARTESIAN_POINT ( 'NONE',  ( -12.25000000000000178, 9.850000000011133849, -50.25000000000000711 ) ) ;
#14177=B_SPLINE_CURVE_WITH_KNOTS ( 'NONE', 3,
 ( #199815, #21190, #100652, #180241, #1575, #81107, #160700, #170985, #127963, #147519 ),
 .UNSPECIFIED., .F., .F.,
 ( 4, 3, 3, 4 ),
 ( -2.000561356210515597E-06, 0.000000000000000000, 1.787822682428821068E-05, 4.206475347089863842E-05 ),
 .UNSPECIFIED. ) ;
#14450=LINE ( 'NONE', #172260, #245128 ) ;
#14742=CARTESIAN_POINT ( 'NONE',  ( 13.43663047529820176, 9.446645344706402270, -51.91080645610020383 ) ) ;
#15325=CARTESIAN_POINT ( 'NONE',  ( -16.93302609847409457, 9.996682520814371031, -46.08638849536255577 ) ) ;
#15386=B_SPLINE_CURVE_WITH_KNOTS ( 'NONE', 3,
 ( #120616, #223524, #25371, #81430, #43632, #104838, #145275, #161011, #240542, #220962 ),
 .UNSPECIFIED., .F., .F.,
 ( 4, 3, 3, 4 ),
 ( 7.632826238683908479E-06, 4.756916949875625587E-05, 9.484459048150416206E-05, 0.0001435500935099911655 ),
 .UNSPECIFIED. ) ;
#15657=LINE ( 'NONE', #232121, #27734 ) ;
#15926=DIRECTION ( 'NONE',  ( -1.000000000000000000, 1.652117596168391700E-15, 0.000000000000000000 ) ) ;
#15993=ORIENTED_EDGE ( 'NONE', *, *, #164644, .T. ) ;
#16241=CARTESIAN_POINT ( 'NONE',  ( -16.97092634996618443, 10.00088896635888958, -54.36985723370199253 ) ) ;
#16471=ADVANCED_FACE ( 'NONE', ( #58454 ), #57170, .F. ) ;
#16510=CIRCLE ( 'NONE', #245467, 0.1000000000000001305 ) ;
#16531=DIRECTION ( 'NONE',  ( 1.000000000000000000, 0.000000000000000000, 0.000000000000000000 ) ) ;
#16558=FACE_OUTER_BOUND ( 'NONE', #41911, .T. ) ;
#16636=CARTESIAN_POINT ( 'NONE',  ( -16.92778301347281911, 10.00094491684643927, -46.07148189203164890 ) ) ;
#16799=CARTESIAN_POINT ( 'NONE',  ( -17.11825945287482753, 9.950000000011138823, -46.25000000000000000 ) ) ;
#17025=EDGE_CURVE ( 'NONE', #143756, #165658, #253090, .T. ) ;
#17294=CARTESIAN_POINT ( 'NONE',  ( 13.12229106158772751, 9.430637101707892711, -51.76826061806093549 ) ) ;
#17809=CARTESIAN_POINT ( 'NONE',  ( -16.89935556175677789, 9.950000000011137047, -46.63967636288582241 ) ) ;
#18184=DIRECTION ( 'NONE',  ( -0.000000000000000000, -0.000000000000000000, -1.000000000000000000 ) ) ;
#18205=CARTESIAN_POINT ( 'NONE',  ( -17.27223548802641062, 10.34539739141212955, -55.63360617919391160 ) ) ;
#18300=ORIENTED_EDGE ( 'NONE', *, *, #92092, .F. ) ;
#18515=EDGE_CURVE ( 'NONE', #141210, #27482, #81330, .T. ) ;
#18528=CARTESIAN_POINT ( 'NONE',  ( -14.11361717019515538, 9.457426452500055092, -52.00004186840004650 ) ) ;
#18769=CARTESIAN_POINT ( 'NONE',  ( -17.11825945287481687, 10.05000000001113847, -54.35000000000000853 ) ) ;
#18819=DIRECTION ( 'NONE',  ( -0.000000000000000000, -0.000000000000000000, -1.000000000000000000 ) ) ;
#19100=CARTESIAN_POINT ( 'NONE',  ( -16.97683809663752186, 9.950000000011137047, -46.90236401819648648 ) ) ;
#19389=LINE ( 'NONE', #98883, #199814 ) ;
#19831=CARTESIAN_POINT ( 'NONE',  ( -15.51798037960204901, 9.376659938544690931, -51.12819254821731363 ) ) ;
#19918=EDGE_CURVE ( 'NONE', #126571, #936, #216994, .T. ) ;
#20189=ORIENTED_EDGE ( 'NONE', *, *, #253155, .T. ) ;
#20253=DIRECTION ( 'NONE',  ( 1.000000000000000000, 0.000000000000000000, -0.000000000000000000 ) ) ;
#20268=CARTESIAN_POINT ( 'NONE',  ( -16.94445028196808778, 9.992063609708889516, -46.10733017841845793 ) ) ;
#20274=LINE ( 'NONE', #257523, #163756 ) ;
#20418=EDGE_LOOP ( 'NONE', ( #226591, #22217, #144584, #204682, #109154, #121090 ) ) ;
#20441=CARTESIAN_POINT ( 'NONE',  ( 13.99999999999999822, 9.850000000011137402, -50.24999999999999289 ) ) ;
#20504=ORIENTED_EDGE ( 'NONE', *, *, #223855, .T. ) ;
#20588=B_SPLINE_CURVE_WITH_KNOTS ( 'NONE', 3,
 ( #188350, #5835, #227462, #164932, #249619, #65827, #28024, #170121, #224887, #107521, #150519, #205321, #207936, #187088, #8437, #87937, #9703, #26732, #106218, #185780, #7130, #86648, #173979, #113941, #31873, #33171 ),
 .UNSPECIFIED., .F., .F.,
 ( 4, 2, 2, 2, 2, 2, 2, 2, 2, 2, 2, 2, 4 ),
 ( 0.005476422646581341307, 0.006160811967703542710, 0.006845201288825743247, 0.007187395949386851321, 0.007529590609947959395, 0.007871785270509067470, 0.008213979931070175544, 0.008556174591631281884, 0.008898369252192389958, 0.009240563912753498033, 0.009582758573314606107, 0.01026714789443682226, 0.01095153721555903667 ),
 .UNSPECIFIED. ) ;
#20798=VERTEX_POINT ( 'NONE', #93739 ) ;
#20875=FACE_OUTER_BOUND ( 'NONE', #34750, .T. ) ;
#20990=VERTEX_POINT ( 'NONE', #209522 ) ;
#21049=CARTESIAN_POINT ( 'NONE',  ( -18.37013991200266005, 11.49974761622312691, -42.70697698948288945 ) ) ;
#21081=CARTESIAN_POINT ( 'NONE',  ( 20.05000000000002913, 7.250000000011171508, -46.15000000000000568 ) ) ;
#21095=ORIENTED_EDGE ( 'NONE', *, *, #156645, .F. ) ;
#21190=CARTESIAN_POINT ( 'NONE',  ( -16.77732147262506146, 9.945966932629787038, -54.33649124327587998 ) ) ;
#21223=VERTEX_POINT ( 'NONE', #50131 ) ;
#21330=CARTESIAN_POINT ( 'NONE',  ( -18.35235881385853318, 11.47341900772405054, -42.75000000000000000 ) ) ;
#21444=ORIENTED_EDGE ( 'NONE', *, *, #230399, .F. ) ;
#21502=EDGE_LOOP ( 'NONE', ( #63227, #27249, #217470, #34133 ) ) ;
#21575=CARTESIAN_POINT ( 'NONE',  ( -18.40000000000000213, 11.75000000001113953, -57.75000000000000711 ) ) ;
#21668=VERTEX_POINT ( 'NONE', #182950 ) ;
#21954=AXIS2_PLACEMENT_3D ( 'NONE', #247227, #68611, #108998 ) ;
#22018=CARTESIAN_POINT ( 'NONE',  ( -16.94107738177415712, 10.01423928514777728, -46.04999999999999716 ) ) ;
#22095=VERTEX_POINT ( 'NONE', #1550 ) ;
#22217=ORIENTED_EDGE ( 'NONE', *, *, #237240, .T. ) ;
#22518=STYLED_ITEM ( 'NONE', ( #43559 ), #25658 ) ;
#22734=ORIENTED_EDGE ( 'NONE', *, *, #230399, .T. ) ;
#22874=CARTESIAN_POINT ( 'NONE',  ( -15.15766958671843589, 9.410538608540020888, -48.93268799714089567 ) ) ;
#23025=CARTESIAN_POINT ( 'NONE',  ( -17.71734398241073549, 10.84235722847571637, -56.72513825300558921 ) ) ;
#23398=DIRECTION ( 'NONE',  ( -0.000000000000000000, -0.000000000000000000, -1.000000000000000000 ) ) ;
#23480=EDGE_CURVE ( 'NONE', #131288, #199985, #15386, .T. ) ;
#23610=CARTESIAN_POINT ( 'NONE',  ( -21.65000000000000213, 9.950000000011140600, -46.25000000000000711 ) ) ;
#23638=VECTOR ( 'NONE', #87132, 1000.000000000000000 ) ;
#23738=ORIENTED_EDGE ( 'NONE', *, *, #55589, .F. ) ;
#23965=VECTOR ( 'NONE', #70528, 1000.000000000000000 ) ;
#24020=DIRECTION ( 'NONE',  ( -0.7071067811865487940, 0.7071067811865463515, -7.215498431451184074E-16 ) ) ;
#24388=DIRECTION ( 'NONE',  ( 0.7071067811865487940, 0.7071067811865462405, -7.215498431451186046E-16 ) ) ;
#24475=EDGE_CURVE ( 'NONE', #63272, #104591, #198256, .T. ) ;
#24642=CARTESIAN_POINT ( 'NONE',  ( -16.91247567987037925, 9.959082683680399839, -46.12872445853733439 ) ) ;
#24812=DIRECTION ( 'NONE',  ( 0.000000000000000000, 0.000000000000000000, 1.000000000000000000 ) ) ;
#24910=EDGE_CURVE ( 'NONE', #20990, #129691, #7445, .T. ) ;
#24997=EDGE_CURVE ( 'NONE', #152757, #936, #153429, .T. ) ;
#25286=EDGE_CURVE ( 'NONE', #227367, #201931, #20588, .T. ) ;
#25371=CARTESIAN_POINT ( 'NONE',  ( -16.87786941232801041, 9.958154714156124854, -54.37718579979401312 ) ) ;
#25462=ORIENTED_EDGE ( 'NONE', *, *, #53876, .F. ) ;
#25586=LINE ( 'NONE', #125942, #53600 ) ;
#25658=MANIFOLD_SOLID_BREP ( 'Stock-MAS-200-1', #136839 ) ;
#25781=EDGE_LOOP ( 'NONE', ( #199942, #124515, #255965, #239378 ) ) ;
#25916=LINE ( 'NONE', #49314, #87215 ) ;
#25973=CARTESIAN_POINT ( 'NONE',  ( -23.25000000000000355, 5.650000000011139001, -46.15000000000000568 ) ) ;
#26210=CARTESIAN_POINT ( 'NONE',  ( -16.88593481969334320, 9.950560090095464716, -54.35187225694449609 ) ) ;
#26575=SURFACE_SIDE_STYLE ('',( #239182 ) ) ;
#26586=FACE_OUTER_BOUND ( 'NONE', #77724, .T. ) ;
#26683=EDGE_CURVE ( 'NONE', #123176, #102761, #109957, .T. ) ;
#26732=CARTESIAN_POINT ( 'NONE',  ( 14.77516762759921498, 9.436674251854011430, -48.67686193099920899 ) ) ;
#26818=VERTEX_POINT ( 'NONE', #107416 ) ;
#26822=CARTESIAN_POINT ( 'NONE',  ( -16.89268316805466341, 9.951721813253341153, -46.14424752145445296 ) ) ;
#26940=FACE_OUTER_BOUND ( 'NONE', #58524, .T. ) ;
#26956=CARTESIAN_POINT ( 'NONE',  ( -16.80438519320023616, 9.949779096479501206, -46.15073828092127428 ) ) ;
#26972=LINE ( 'NONE', #84283, #85422 ) ;
#27033=EDGE_CURVE ( 'NONE', #21223, #20798, #156853, .T. ) ;
#27128=EDGE_CURVE ( 'NONE', #123899, #192971, #180887, .T. ) ;
#27249=ORIENTED_EDGE ( 'NONE', *, *, #92092, .T. ) ;
#27377=CARTESIAN_POINT ( 'NONE',  ( -17.29158576265543346, 10.36474766602906783, -55.58275824479218130 ) ) ;
#27418=EDGE_LOOP ( 'NONE', ( #165407, #91739, #105985, #172968 ) ) ;
#27457=CARTESIAN_POINT ( 'NONE',  ( -16.92989507731676824, 9.950000000011140600, -54.11749893061020344 ) ) ;
#27482=VERTEX_POINT ( 'NONE', #69936 ) ;
#27640=DIRECTION ( 'NONE',  ( -1.073024830501117725E-15, 0.000000000000000000, 1.000000000000000000 ) ) ;
#27734=VECTOR ( 'NONE', #235943, 1000.000000000000000 ) ;
#27850=VERTEX_POINT ( 'NONE', #132154 ) ;
#27938=DIRECTION ( 'NONE',  ( 1.186688945009009831E-16, -1.000000000000000000, 0.000000000000000000 ) ) ;
#28013=CARTESIAN_POINT ( 'NONE',  ( -12.93407622233968901, 9.417789466963363054, -48.85738454397688457 ) ) ;
#28024=CARTESIAN_POINT ( 'NONE',  ( 12.93225390519045526, 9.417651958852164995, -48.85878739244044056 ) ) ;
#28346=AXIS2_PLACEMENT_3D ( 'NONE', #58509, #138052, #234599 ) ;
#28462=ORIENTED_EDGE ( 'NONE', *, *, #173952, .T. ) ;
#28649=ORIENTED_EDGE ( 'NONE', *, *, #60456, .T. ) ;
#28680=DIRECTION ( 'NONE',  ( 0.000000000000000000, 0.000000000000000000, 1.000000000000000000 ) ) ;
#28700=DIRECTION ( 'NONE',  ( -0.5932847527679299127, 0.8049926720990051576, 6.366092712777055223E-16 ) ) ;
#28730=ORIENTED_EDGE ( 'NONE', *, *, #42938, .F. ) ;
#28893=DIRECTION ( 'NONE',  ( -0.000000000000000000, -0.000000000000000000, -1.000000000000000000 ) ) ;
#28974=CARTESIAN_POINT ( 'NONE',  ( -17.11825945287482753, 10.05000000001113847, -46.15000000000000568 ) ) ;
#29005=CARTESIAN_POINT ( 'NONE',  ( -16.86132326855786090, 9.950000000011133494, -46.19863578466831910 ) ) ;
#29010=DIRECTION ( 'NONE',  ( 0.000000000000000000, 0.000000000000000000, 1.000000000000000000 ) ) ;
#29083=TOROIDAL_SURFACE ( 'NONE', #116534, 14.20833333333334103, 0.1000000000000000056 ) ;
#29126=CARTESIAN_POINT ( 'NONE',  ( -16.88705144915408596, 9.950000000011193890, -54.06902140528774936 ) ) ;
#29305=EDGE_LOOP ( 'NONE', ( #59532, #30026, #52916, #141542 ) ) ;
#29484=EDGE_CURVE ( 'NONE', #149704, #131288, #157165, .T. ) ;
#29532=LINE ( 'NONE', #127316, #138089 ) ;
#29564=ORIENTED_EDGE ( 'NONE', *, *, #141912, .F. ) ;
#29641=ORIENTED_EDGE ( 'NONE', *, *, #172080, .F. ) ;
#29769=CARTESIAN_POINT ( 'NONE',  ( -16.94445028196808778, 9.992063609708889516, -46.10733017841845793 ) ) ;
#29788=ORIENTED_EDGE ( 'NONE', *, *, #184364, .T. ) ;
#29831=DIRECTION ( 'NONE',  ( -0.000000000000000000, 0.000000000000000000, -1.000000000000000000 ) ) ;
#29863=ADVANCED_FACE ( 'NONE', ( #7793 ), #207286, .F. ) ;
#30015=DIRECTION ( 'NONE',  ( 0.7071067811865493491, 0.7071067811865456854, 0.000000000000000000 ) ) ;
#30026=ORIENTED_EDGE ( 'NONE', *, *, #141263, .F. ) ;
#30041=DIRECTION ( 'NONE',  ( 0.000000000000000000, 0.9553114395362780620, -0.2956011730205483912 ) ) ;
#30083=PLANE ( 'NONE',  #50150 ) ;
#30232=CARTESIAN_POINT ( 'NONE',  ( 18.39999999999997371, 11.47316190337362940, -57.75000000000000711 ) ) ;
#30379=CARTESIAN_POINT ( 'NONE',  ( -16.84793658983419107, 9.950000000011138823, -54.26635332218975805 ) ) ;
#30428=ORIENTED_EDGE ( 'NONE', *, *, #6403, .T. ) ;
#30637=CARTESIAN_POINT ( 'NONE',  ( -16.87683809663752399, 9.850000000011144508, -46.90236401819630885 ) ) ;
#31002=ADVANCED_FACE ( 'NONE', ( #204271 ), #225108, .F. ) ;
#31045=LINE ( 'NONE', #190085, #118879 ) ;
#31065=CARTESIAN_POINT ( 'NONE',  ( -16.77683809663752257, 9.950000000011138823, -54.35000000000000142 ) ) ;
#31602=ORIENTED_EDGE ( 'NONE', *, *, #165324, .F. ) ;
#31678=CARTESIAN_POINT ( 'NONE',  ( -16.92280123533709713, 9.950000000011137047, -54.14936768591468308 ) ) ;
#31731=DIRECTION ( 'NONE',  ( -1.000000000000000000, -1.646408749285562691E-14, 0.000000000000000000 ) ) ;
#31873=CARTESIAN_POINT ( 'NONE',  ( 15.74999999999999645, 9.350000000011133849, -50.01856895740262132 ) ) ;
#31880=VECTOR ( 'NONE', #135356, 1000.000000000000000 ) ;
#32042=( GEOMETRIC_REPRESENTATION_CONTEXT ( 3 ) GLOBAL_UNCERTAINTY_ASSIGNED_CONTEXT ( ( #76659 ) ) GLOBAL_UNIT_ASSIGNED_CONTEXT ( ( #152956, #90365, #51213 ) ) REPRESENTATION_CONTEXT ( 'NONE', 'WORKASPACE' ) );
#32051=ORIENTED_EDGE ( 'NONE', *, *, #149409, .T. ) ;
#32165=ORIENTED_EDGE ( 'NONE', *, *, #198863, .T. ) ;
#32210=CARTESIAN_POINT ( 'NONE',  ( -15.55912972643741199, 8.490870273573719373, -46.15000000000000568 ) ) ;
#32213=DIRECTION ( 'NONE',  ( 1.186688945009010077E-16, -1.000000000000000000, -0.000000000000000000 ) ) ;
#32459=CARTESIAN_POINT ( 'NONE',  ( -23.25000000000000355, 11.75000000001113953, -57.75000000000000000 ) ) ;
#32555=EDGE_CURVE ( 'NONE', #132925, #2821, #43958, .T. ) ;
#32664=CARTESIAN_POINT ( 'NONE',  ( -16.86445178670632217, 9.962211629127168067, -54.39077743811736099 ) ) ;
#32899=CARTESIAN_POINT ( 'NONE',  ( -16.94445028196807002, 9.992063609708893068, -54.39266982158155628 ) ) ;
#33072=VECTOR ( 'NONE', #95100, 1000.000000000000000 ) ;
#33171=CARTESIAN_POINT ( 'NONE',  ( 15.74999999999999645, 9.350000000011139178, -50.25000000000000000 ) ) ;
#33259=DIRECTION ( 'NONE',  ( 1.073024830501117725E-15, -0.000000000000000000, -1.000000000000000000 ) ) ;
#33517=DIRECTION ( 'NONE',  ( -0.7071067811865463515, 0.7071067811865487940, -0.000000000000000000 ) ) ;
#33671=DIRECTION ( 'NONE',  ( 0.000000000000000000, 0.000000000000000000, 1.000000000000000000 ) ) ;
#33823=FACE_OUTER_BOUND ( 'NONE', #174016, .T. ) ;
#33886=PLANE ( 'NONE',  #160873 ) ;
#34063=EDGE_CURVE ( 'NONE', #104591, #149704, #214836, .T. ) ;
#34113=CARTESIAN_POINT ( 'NONE',  ( -16.94389599337535657, 9.991197989767881538, -54.39235519820161358 ) ) ;
#34133=ORIENTED_EDGE ( 'NONE', *, *, #68118, .T. ) ;
#34180=CARTESIAN_POINT ( 'NONE',  ( 20.99999999999999645, 9.750000000011137757, -42.75000000000000000 ) ) ;
#34367=ORIENTED_EDGE ( 'NONE', *, *, #84734, .F. ) ;
#34491=CARTESIAN_POINT ( 'NONE',  ( -16.88560720703333473, 9.950564843760847822, -46.14811192086371960 ) ) ;
#34750=EDGE_LOOP ( 'NONE', ( #251954, #173884, #228157, #99097 ) ) ;
#34900=CARTESIAN_POINT ( 'NONE',  ( -16.93970660449832621, 10.01284139164672915, -46.05228173579446604 ) ) ;
#34937=FACE_OUTER_BOUND ( 'NONE', #109719, .T. ) ;
#35394=CARTESIAN_POINT ( 'NONE',  ( -16.94165728009537375, 9.987869755934930538, -54.39105500851019315 ) ) ;
#35590=CARTESIAN_POINT ( 'NONE',  ( 12.24999999999999467, 9.350000000011135626, -50.36426760761606403 ) ) ;
#35797=CARTESIAN_POINT ( 'NONE',  ( -16.91049119928363353, 9.950000000011138823, -54.38172039319083240 ) ) ;
#35815=LINE ( 'NONE', #176608, #61065 ) ;
#35924=AXIS2_PLACEMENT_3D ( 'NONE', #34180, #113677, #109817 ) ;
#36228=ORIENTED_EDGE ( 'NONE', *, *, #213195, .T. ) ;
#36254=DIRECTION ( 'NONE',  ( -0.000000000000000000, -0.000000000000000000, -1.000000000000000000 ) ) ;
#36842=CARTESIAN_POINT ( 'NONE',  ( -12.60829076262179527, 9.389529397477895500, -51.31710791289368956 ) ) ;
#36984=CARTESIAN_POINT ( 'NONE',  ( -21.64999999999999858, 10.05000000001113847, -54.35000000000000142 ) ) ;
#37049=ORIENTED_EDGE ( 'NONE', *, *, #246193, .F. ) ;
#37407=CARTESIAN_POINT ( 'NONE',  ( -16.87683809663750978, 9.950000000011137047, -46.90236401819647227 ) ) ;
#37790=CARTESIAN_POINT ( 'NONE',  ( -16.87036670365548474, 9.989418819312799513, -54.47956011730205006 ) ) ;
#37946=CARTESIAN_POINT ( 'NONE',  ( -16.92563707711778065, 9.968990694407935393, -54.38075829952398266 ) ) ;
#37967=CARTESIAN_POINT ( 'NONE',  ( -16.79140778683510149, 9.944941598865719712, -54.32973723377079978 ) ) ;
#38104=CARTESIAN_POINT ( 'NONE',  ( -15.31895204843005409, 9.396533993965080711, -51.40593977917331614 ) ) ;
#38409=AXIS2_PLACEMENT_3D ( 'NONE', #5903, #202836, #108874 ) ;
#38596=DIRECTION ( 'NONE',  ( 1.073024830501117725E-15, -0.000000000000000000, -1.000000000000000000 ) ) ;
#38676=CARTESIAN_POINT ( 'NONE',  ( -16.83233564386402037, 9.930221796595741779, -46.27547933652439838 ) ) ;
#38758=CARTESIAN_POINT ( 'NONE',  ( -16.92570016628985030, 9.958788957751016468, -46.12065067003899799 ) ) ;
#38836=EDGE_CURVE ( 'NONE', #247898, #129691, #129531, .T. ) ;
#38922=CARTESIAN_POINT ( 'NONE',  ( -16.93388492042258875, 9.988541822527059466, -46.09945487681383014 ) ) ;
#39171=LINE ( 'NONE', #76980, #257180 ) ;
#39234=CARTESIAN_POINT ( 'NONE',  ( -16.94052228080551359, 9.986279733109993728, -54.39037550266942844 ) ) ;
#39364=B_SPLINE_CURVE_WITH_KNOTS ( 'NONE', 3,
 ( #247107, #128462, #245842, #68493, #243253, #148028, #69790, #228851, #48913, #26822 ),
 .UNSPECIFIED., .F., .F.,
 ( 4, 3, 3, 4 ),
 ( 0.000000000000000000, 4.874959354401679605E-05, 9.785140065120807406E-05, 0.0001360444631935947134 ),
 .UNSPECIFIED. ) ;
#39403=ORIENTED_EDGE ( 'NONE', *, *, #125401, .T. ) ;
#39558=LINE ( 'NONE', #241569, #153405 ) ;
#39574=CARTESIAN_POINT ( 'NONE',  ( -16.97683809663753252, 9.950000000011140600, -46.77152476866995556 ) ) ;
#39748=ORIENTED_EDGE ( 'NONE', *, *, #164623, .F. ) ;
#39821=ORIENTED_EDGE ( 'NONE', *, *, #257839, .F. ) ;
#39987=CARTESIAN_POINT ( 'NONE',  ( -16.82055514392384765, 9.950000000011135270, -46.17679807454214114 ) ) ;
#40205=CARTESIAN_POINT ( 'NONE',  ( -16.93589915522259304, 10.00862525870701170, -54.44056010196031536 ) ) ;
#40469=DIRECTION ( 'NONE',  ( 1.000000000000000000, -0.000000000000000000, -0.000000000000000000 ) ) ;
#40566=VERTEX_POINT ( 'NONE', #117401 ) ;
#40957=DIRECTION ( 'NONE',  ( 1.000000000000000000, 0.000000000000000000, 0.000000000000000000 ) ) ;
#41192=DIRECTION ( 'NONE',  ( -1.000000000000000000, 0.000000000000000000, 0.000000000000000000 ) ) ;
#41217=CARTESIAN_POINT ( 'NONE',  ( -16.81453046979149590, 9.939102281452072418, -46.21172652360304767 ) ) ;
#41532=CARTESIAN_POINT ( 'NONE',  ( -16.87036670365549895, 9.989418819312803066, -46.02043988269794994 ) ) ;
#41709=DIRECTION ( 'NONE',  ( 0.000000000000000000, 0.000000000000000000, -1.000000000000000000 ) ) ;
#41911=EDGE_LOOP ( 'NONE', ( #20504, #129857, #154406, #34367 ) ) ;
#42080=EDGE_CURVE ( 'NONE', #191054, #201931, #183310, .T. ) ;
#42420=DIRECTION ( 'NONE',  ( 0.8049926720990051576, 0.5932847527679298016, -0.000000000000000000 ) ) ;
#42479=( BOUNDED_CURVE ( )  B_SPLINE_CURVE ( 3, ( #226302, #45125, #23025, #145499 ),
 .UNSPECIFIED., .F., .F. ) 
 B_SPLINE_CURVE_WITH_KNOTS ( ( 4, 4 ),
 ( 0.3000847527772389500, 0.5517402753107879532 ),
 .UNSPECIFIED. ) 
 CURVE ( )  GEOMETRIC_REPRESENTATION_ITEM ( )  RATIONAL_B_SPLINE_CURVE ( ( 1.000000000000000000, 0.9947294176030464508, 0.9947294176030464508, 1.000000000000000000 ) ) 
 REPRESENTATION_ITEM ( '' )  );
#42689=ORIENTED_EDGE ( 'NONE', *, *, #207552, .T. ) ;
#42737=CARTESIAN_POINT ( 'NONE',  ( -16.93415306273742260, 9.995622260023671046, -54.41005694236041990 ) ) ;
#42813=ORIENTED_EDGE ( 'NONE', *, *, #240143, .F. ) ;
#42895=LINE ( 'NONE', #31065, #23638 ) ;
#42938=EDGE_CURVE ( 'NONE', #53148, #129691, #232267, .T. ) ;
#43139=ORIENTED_EDGE ( 'NONE', *, *, #72524, .F. ) ;
#43211=CARTESIAN_POINT ( 'NONE',  ( 21.72449340488910607, 10.28395627750226815, -54.34999999999999432 ) ) ;
#43352=CARTESIAN_POINT ( 'NONE',  ( 21.13736287352038445, 8.046642376395153562, -46.15000000000000568 ) ) ;
#43559=PRESENTATION_STYLE_ASSIGNMENT (( #85204 ) ) ;
#43598=VERTEX_POINT ( 'NONE', #159638 ) ;
#43632=CARTESIAN_POINT ( 'NONE',  ( -16.86733706339143524, 9.965990529650820662, -54.40311530199869594 ) ) ;
#43671=ORIENTED_EDGE ( 'NONE', *, *, #141263, .T. ) ;
#43755=CARTESIAN_POINT ( 'NONE',  ( -16.81930730667006557, 9.936998068885202429, -46.22676773053819943 ) ) ;
#43809=ORIENTED_EDGE ( 'NONE', *, *, #82601, .F. ) ;
#43892=CARTESIAN_POINT ( 'NONE',  ( 14.88075390448863899, 9.431689550535253375, -51.77929003223604809 ) ) ;
#43958=CIRCLE ( 'NONE', #160711, 1.500000000000001332 ) ;
#44028=CIRCLE ( 'NONE', #177347, 14.30833333333333890 ) ;
#44187=CARTESIAN_POINT ( 'NONE',  ( -16.90257928357874917, 9.954106821116520010, -46.13628543011370198 ) ) ;
#44603=AXIS2_PLACEMENT_3D ( 'NONE', #167442, #27938, #107437 ) ;
#44738=ORIENTED_EDGE ( 'NONE', *, *, #42938, .T. ) ;
#44812=LINE ( 'NONE', #46081, #167396 ) ;
#44835=( NAMED_UNIT ( * ) SI_UNIT ( $, .STERADIAN. ) SOLID_ANGLE_UNIT ( ) );
#44905=EDGE_CURVE ( 'NONE', #144797, #63272, #123217, .T. ) ;
#44939=EDGE_CURVE ( 'NONE', #119072, #2821, #133398, .T. ) ;
#44982=CARTESIAN_POINT ( 'NONE',  ( -15.75000000000001066, 9.350000000011139178, -50.02151937182511432 ) ) ;
#45125=CARTESIAN_POINT ( 'NONE',  ( -17.22361732159831504, 10.34515565861359043, -55.62921547413287726 ) ) ;
#45127=EDGE_LOOP ( 'NONE', ( #116874, #103724, #91247, #22734 ) ) ;
#45335=AXIS2_PLACEMENT_3D ( 'NONE', #246887, #24020, #223465 ) ;
#45517=DIRECTION ( 'NONE',  ( 1.000000000000000000, 0.000000000000000000, 0.000000000000000000 ) ) ;
#45856=DIRECTION ( 'NONE',  ( 0.000000000000000000, 1.000000000000000000, 3.418575295766609984E-15 ) ) ;
#46062=CARTESIAN_POINT ( 'NONE',  ( -16.97683809663752186, 9.950000000011137047, -53.59763598180368405 ) ) ;
#46081=CARTESIAN_POINT ( 'NONE',  ( 20.73486653747088582, 7.250000000011182166, -42.75000000000000000 ) ) ;
#46158=DIRECTION ( 'NONE',  ( -1.000000000000000000, 1.652117596168391700E-15, 0.000000000000000000 ) ) ;
#46182=ORIENTED_EDGE ( 'NONE', *, *, #141471, .T. ) ;
#46201=AXIS2_PLACEMENT_3D ( 'NONE', #149705, #87121, #148402 ) ;
#46305=CARTESIAN_POINT ( 'NONE',  ( -18.40000000000000213, 11.41458325961095177, -54.34999999999999432 ) ) ;
#46396=ADVANCED_FACE ( 'NONE', ( #49367 ), #251412, .F. ) ;
#46884=CARTESIAN_POINT ( 'NONE',  ( -18.40000000000000213, 11.75000000001113953, -54.35000000000000142 ) ) ;
#46951=CARTESIAN_POINT ( 'NONE',  ( -16.90138253750127006, 9.950000000011138823, -54.21156270790459075 ) ) ;
#47133=VERTEX_POINT ( 'NONE', #226073 ) ;
#47249=DIRECTION ( 'NONE',  ( -0.000000000000000000, -0.000000000000000000, -1.000000000000000000 ) ) ;
#47689=DIRECTION ( 'NONE',  ( 1.000000000000000000, 0.000000000000000000, -0.000000000000000000 ) ) ;
#47719=VERTEX_POINT ( 'NONE', #140828 ) ;
#47928=VECTOR ( 'NONE', #217463, 1000.000000000000000 ) ;
#48113=EDGE_LOOP ( 'NONE', ( #8678, #23738, #67150, #31602 ) ) ;
#48321=CARTESIAN_POINT ( 'NONE',  ( -16.88328101497759448, 9.950352834230013599, -54.35117951492927801 ) ) ;
#48575=COLOUR_RGB ( '', 0.40784314, 0.44705882, 0.49803922) ;
#48628=CARTESIAN_POINT ( 'NONE',  ( -16.87401514999234209, 9.950000000011137047, -54.28001799253208759 ) ) ;
#48644=ORIENTED_EDGE ( 'NONE', *, *, #227533, .F. ) ;
#48913=CARTESIAN_POINT ( 'NONE',  ( -16.88495309932522659, 9.954627058484012636, -46.13454867381192059 ) ) ;
#49314=CARTESIAN_POINT ( 'NONE',  ( 20.73486653747090003, 7.250000000011182166, -54.35000000000000142 ) ) ;
#49337=CIRCLE ( 'NONE', #7657, 0.09999999999999939493 ) ;
#49361=VECTOR ( 'NONE', #50921, 1000.000000000000000 ) ;
#49367=FACE_OUTER_BOUND ( 'NONE', #192602, .T. ) ;
#49800=ORIENTED_EDGE ( 'NONE', *, *, #149989, .T. ) ;
#49861=EDGE_CURVE ( 'NONE', #247898, #120029, #91208, .T. ) ;
#49918=CARTESIAN_POINT ( 'NONE',  ( -16.77431908686106254, 9.945805754529134290, -54.33583921765023916 ) ) ;
#49985=EDGE_CURVE ( 'NONE', #150648, #248438, #89764, .T. ) ;
#50076=LINE ( 'NONE', #129623, #92110 ) ;
#50131=CARTESIAN_POINT ( 'NONE',  ( -18.40000000000000213, 11.75000000001113953, -46.15000000000000568 ) ) ;
#50150=AXIS2_PLACEMENT_3D ( 'NONE', #126587, #147433, #125309 ) ;
#50630=DIRECTION ( 'NONE',  ( -0.000000000000000000, -0.000000000000000000, -1.000000000000000000 ) ) ;
#50921=DIRECTION ( 'NONE',  ( 1.000000000000000000, -0.000000000000000000, -0.000000000000000000 ) ) ;
#50955=VERTEX_POINT ( 'NONE', #139509 ) ;
#50985=CARTESIAN_POINT ( 'NONE',  ( -18.39999999999999858, 11.47316190337362762, -42.82594606680797256 ) ) ;
#51213=( NAMED_UNIT ( * ) SI_UNIT ( $, .STERADIAN. ) SOLID_ANGLE_UNIT ( ) );
#51461=ORIENTED_EDGE ( 'NONE', *, *, #184211, .F. ) ;
#51598=ORIENTED_EDGE ( 'NONE', *, *, #237240, .F. ) ;
#51951=EDGE_CURVE ( 'NONE', #127380, #149877, #50076, .T. ) ;
#52084=VECTOR ( 'NONE', #33517, 1000.000000000000000 ) ;
#52406=CYLINDRICAL_SURFACE ( 'NONE', #35924, 0.9000000000000014655 ) ;
#52516=SURFACE_SIDE_STYLE ('',( #231193 ) ) ;
#52540=CARTESIAN_POINT ( 'NONE',  ( 15.69410316191958898, 9.356746017089401235, -50.70335972136417979 ) ) ;
#52574=EDGE_LOOP ( 'NONE', ( #191339, #197002, #244859 ) ) ;
#52768=CARTESIAN_POINT ( 'NONE',  ( -16.92507428761701505, 9.950000000011138823, -46.21339745962156087 ) ) ;
#52893=VERTEX_POINT ( 'NONE', #62073 ) ;
#52916=ORIENTED_EDGE ( 'NONE', *, *, #174264, .F. ) ;
#53148=VERTEX_POINT ( 'NONE', #73653 ) ;
#53348=LINE ( 'NONE', #12965, #218787 ) ;
#53465=CARTESIAN_POINT ( 'NONE',  ( -16.92570016628983609, 9.958788957751018245, -54.37934932996099491 ) ) ;
#53469=FACE_OUTER_BOUND ( 'NONE', #209082, .T. ) ;
#53600=VECTOR ( 'NONE', #105064, 1000.000000000000000 ) ;
#53637=CARTESIAN_POINT ( 'NONE',  ( -16.91776028072577631, 9.963400393640901243, -54.37502401470212732 ) ) ;
#53816=FILL_AREA_STYLE_COLOUR ( '', #48575 ) ;
#53876=EDGE_CURVE ( 'NONE', #169303, #73622, #229213, .T. ) ;
#53945=ADVANCED_FACE ( 'NONE', ( #214764 ), #159956, .F. ) ;
#54270=ORIENTED_EDGE ( 'NONE', *, *, #5973, .F. ) ;
#54271=B_SPLINE_CURVE_WITH_KNOTS ( 'NONE', 3,
 ( #220784, #143801, #180385, #138644, #21330, #83794, #163389 ),
 .UNSPECIFIED., .F., .F.,
 ( 4, 3, 4 ),
 ( 0.000000000000000000, 4.520325912680675046E-05, 5.794988040901435228E-05 ),
 .UNSPECIFIED. ) ;
#54433=ORIENTED_EDGE ( 'NONE', *, *, #221160, .T. ) ;
#54650=VECTOR ( 'NONE', #161647, 1000.000000000000000 ) ;
#54957=EDGE_LOOP ( 'NONE', ( #106052, #211774, #176922, #199499 ) ) ;
#55273=CARTESIAN_POINT ( 'NONE',  ( -16.87383368123029825, 9.950000000011138823, -46.15000000000000568 ) ) ;
#55419=( BOUNDED_SURFACE ( )  B_SPLINE_SURFACE ( 3, 2, ( 
 ( #214403, #35797, #257327 ),
 ( #155758, #115304, #16241 ),
 ( #218240, #95731, #175320 ),
 ( #479, #254771, #18769 ) ),
 .UNSPECIFIED., .F., .F., .F. ) 
 B_SPLINE_SURFACE_WITH_KNOTS ( ( 4, 4 ),
 ( 3, 3 ),
 ( 3.658908243880901523, 4.712388980384689674 ),
 ( 0.000000000000000000, 1.000000000000000000 ),
 .UNSPECIFIED. ) 
 GEOMETRIC_REPRESENTATION_ITEM ( )  RATIONAL_B_SPLINE_SURFACE ( (
 ( 1.000000000000000000, 0.8984936768950558816, 1.000000000000000000),
 ( 1.000000000000000000, 0.8646876308615779605, 1.000000000000000000),
 ( 1.000000000000000000, 0.7953136715912922927, 1.000000000000000000),
 ( 1.000000000000000000, 0.7071067811865719976, 1.000000000000000000) ) ) 
 REPRESENTATION_ITEM ( '' )  SURFACE ( )  );
#55589=EDGE_CURVE ( 'NONE', #192971, #123899, #243047, .T. ) ;
#56346=CARTESIAN_POINT ( 'NONE',  ( -14.45422546970484667, 9.450602096099681049, -51.94389596309667922 ) ) ;
#56474=LINE ( 'NONE', #215563, #195083 ) ;
#56599=CARTESIAN_POINT ( 'NONE',  ( 18.39999999999999503, 11.75000000001113953, -46.15000000000000568 ) ) ;
#57151=CARTESIAN_POINT ( 'NONE',  ( 23.24999999999999645, 11.75000000001113953, -46.15000000000001279 ) ) ;
#57170=PLANE ( 'NONE',  #227906 ) ;
#57226=CARTESIAN_POINT ( 'NONE',  ( -18.40000000000000213, 11.48667500176882328, -42.75000000000000000 ) ) ;
#57375=LINE ( 'NONE', #233489, #231057 ) ;
#57686=CARTESIAN_POINT ( 'NONE',  ( -18.40000000000000213, 11.47867410001105881, -57.72530678365939849 ) ) ;
#57835=CARTESIAN_POINT ( 'NONE',  ( -14.00000000000000178, 9.850000000011133849, -50.25000000000000711 ) ) ;
#58138=LINE ( 'NONE', #198951, #148421 ) ;
#58210=CARTESIAN_POINT ( 'NONE',  ( -16.85697194749129579, 9.908543714134824043, -46.43500426761385569 ) ) ;
#58243=AXIS2_PLACEMENT_3D ( 'NONE', #114027, #33259, #137436 ) ;
#58440=CARTESIAN_POINT ( 'NONE',  ( -21.64999999999999858, 9.350000000011133849, -54.35000000000000142 ) ) ;
#58454=FACE_OUTER_BOUND ( 'NONE', #168574, .T. ) ;
#58509=CARTESIAN_POINT ( 'NONE',  ( 13.99999999999999822, 9.850000000011137402, -50.24999999999999289 ) ) ;
#58524=EDGE_LOOP ( 'NONE', ( #206739, #215376, #200682, #131279 ) ) ;
#58593=DIRECTION ( 'NONE',  ( -1.073024830501117725E-15, -0.000000000000000000, -1.000000000000000000 ) ) ;
#58596=AXIS2_PLACEMENT_3D ( 'NONE', #5461, #86282, #165868 ) ;
#58738=CARTESIAN_POINT ( 'NONE',  ( -16.93301857435212909, 9.976309354746611291, -54.38577557116142458 ) ) ;
#58841=DIRECTION ( 'NONE',  ( 0.000000000000000000, -1.000000000000000000, 0.000000000000000000 ) ) ;
#58901=CARTESIAN_POINT ( 'NONE',  ( -13.77083647240106501, 9.457410930301318075, -51.99991590874629566 ) ) ;
#58915=( LENGTH_UNIT ( ) NAMED_UNIT ( * ) SI_UNIT ( .MILLI., .METRE. ) );
#59027=CARTESIAN_POINT ( 'NONE',  ( 20.27550659511089037, 9.216043722519994930, -54.35000000000000142 ) ) ;
#59093=VECTOR ( 'NONE', #243169, 1000.000000000000000 ) ;
#59532=ORIENTED_EDGE ( 'NONE', *, *, #250118, .F. ) ;
#59558=ORIENTED_EDGE ( 'NONE', *, *, #49985, .F. ) ;
#59587=B_SPLINE_CURVE_WITH_KNOTS ( 'NONE', 3,
 ( #197312, #39574, #98185, #78644, #6829, #85046, #86331, #29005, #108496, #4243 ),
 .UNSPECIFIED., .F., .F.,
 ( 4, 2, 2, 2, 4 ),
 ( 0.000000000000000000, 0.0003916577441626799445, 0.0005874866162440102674, 0.0006854010522846840483, 0.0007833154883253576123 ),
 .UNSPECIFIED. ) ;
#59836=ORIENTED_EDGE ( 'NONE', *, *, #219137, .F. ) ;
#60010=DIRECTION ( 'NONE',  ( -1.000000000000000000, -1.646408749285562691E-14, 1.073024830501117725E-15 ) ) ;
#60061=CARTESIAN_POINT ( 'NONE',  ( -16.83794479845801106, 9.926357419362650703, -54.19644470422232274 ) ) ;
#60102=CARTESIAN_POINT ( 'NONE',  ( 21.13736287352038445, 8.046642376395153562, -54.35000000000000142 ) ) ;
#60131=CARTESIAN_POINT ( 'NONE',  ( -16.91256925476570672, 9.985731158139333985, -46.03235751099471429 ) ) ;
#60207=CARTESIAN_POINT ( 'NONE',  ( -15.69373346032659100, 9.356790025057037496, -50.70482650861391960 ) ) ;
#60337=CARTESIAN_POINT ( 'NONE',  ( -17.04761207306818704, 10.02645087340892616, -54.35000000000000853 ) ) ;
#60456=EDGE_CURVE ( 'NONE', #40566, #247898, #29532, .T. ) ;
#60481=CARTESIAN_POINT ( 'NONE',  ( -18.40000000000000213, 5.650000000011139001, -46.15000000000000568 ) ) ;
#60679=AXIS2_PLACEMENT_3D ( 'NONE', #116847, #38596, #257575 ) ;
#60945=CARTESIAN_POINT ( 'NONE',  ( -21.64999999999999858, 10.05000000001113847, -46.15000000000000568 ) ) ;
#61065=VECTOR ( 'NONE', #77456, 1000.000000000000000 ) ;
#61136=ORIENTED_EDGE ( 'NONE', *, *, #203269, .T. ) ;
#61550=PLANE ( 'NONE',  #6559 ) ;
#61573=EDGE_LOOP ( 'NONE', ( #156513, #252462, #207073, #43671 ) ) ;
#61889=CARTESIAN_POINT ( 'NONE',  ( -20.65000000000000568, 5.650000000011139001, -54.35000000000000142 ) ) ;
#62073=CARTESIAN_POINT ( 'NONE',  ( -16.81744102076749314, 9.950000000011142376, -46.15000000000000568 ) ) ;
#62138=CARTESIAN_POINT ( 'NONE',  ( -16.87683809663752399, 9.850000000011144508, -46.90236401819630885 ) ) ;
#62304=CARTESIAN_POINT ( 'NONE',  ( -16.93353400591625757, 10.00461239618409515, -54.43268447020540890 ) ) ;
#62558=CARTESIAN_POINT ( 'NONE',  ( -18.40000000000000213, 11.41458325961093756, -46.14999999999999858 ) ) ;
#62561=DIRECTION ( 'NONE',  ( 1.186688945009010077E-16, -1.000000000000000000, -0.000000000000000000 ) ) ;
#62722=CARTESIAN_POINT ( 'NONE',  ( -18.41431012584568450, 11.48747202921932598, -42.72676398689832666 ) ) ;
#62771=DIRECTION ( 'NONE',  ( 0.5932847527679299127, -0.8049926720990051576, 6.366092712777055223E-16 ) ) ;
#62879=ORIENTED_EDGE ( 'NONE', *, *, #224617, .F. ) ;
#62934=DIRECTION ( 'NONE',  ( 1.000000000000000000, -0.000000000000000000, -0.000000000000000000 ) ) ;
#63084=DIRECTION ( 'NONE',  ( -1.000000000000000000, 0.000000000000000000, -0.000000000000000000 ) ) ;
#63200=CARTESIAN_POINT ( 'NONE',  ( 23.04999999999999716, 8.822561741677553471, -42.75000000000000000 ) ) ;
#63227=ORIENTED_EDGE ( 'NONE', *, *, #250264, .F. ) ;
#63244=CARTESIAN_POINT ( 'NONE',  ( -14.11697426661281618, 9.457410944778565920, -48.50008397379003355 ) ) ;
#63272=VERTEX_POINT ( 'NONE', #132224 ) ;
#63321=ORIENTED_EDGE ( 'NONE', *, *, #44905, .F. ) ;
#63440=CARTESIAN_POINT ( 'NONE',  ( 15.39170923737819230, 9.389529397477891948, -51.31710791289368245 ) ) ;
#63744=DIRECTION ( 'NONE',  ( 1.000000000000000000, 1.646408749285562691E-14, 1.073024830501117725E-15 ) ) ;
#63828=DIRECTION ( 'NONE',  ( 1.000000000000000000, 0.000000000000000000, 0.000000000000000000 ) ) ;
#64306=CARTESIAN_POINT ( 'NONE',  ( 13.99999999999999822, 9.850000000011137402, -50.24999999999999289 ) ) ;
#64403=FILL_AREA_STYLE_COLOUR ( '', #143296 ) ;
#64536=CARTESIAN_POINT ( 'NONE',  ( -13.12432614554023402, 9.430764995433477793, -48.73053739475046342 ) ) ;
#64579=CARTESIAN_POINT ( 'NONE',  ( -33.72168855820452649, 11.47316190337362585, -42.74999999999999289 ) ) ;
#64603=VECTOR ( 'NONE', #178446, 1000.000000000000000 ) ;
#64612=( BOUNDED_SURFACE ( )  B_SPLINE_SURFACE ( 3, 2, ( 
 ( #199685, #62722, #21049 ),
 ( #138374, #159269, #2724 ),
 ( #238793, #180112, #257014 ),
 ( #219210, #60131, #163121 ) ),
 .UNSPECIFIED., .F., .F., .F. ) 
 B_SPLINE_SURFACE_WITH_KNOTS ( ( 4, 4 ),
 ( 3, 3 ),
 ( 5.727910411845712702, 5.983100554402349225 ),
 ( 0.000000000000000000, 1.000000000000000000 ),
 .UNSPECIFIED. ) 
 GEOMETRIC_REPRESENTATION_ITEM ( )  RATIONAL_B_SPLINE_SURFACE ( (
 ( 1.000000000000000000, 0.8946697475932142707, 1.000000000000000000),
 ( 1.000000000000000000, 0.9035312726220516844, 1.000000000000000000),
 ( 1.000000000000000000, 0.9104333467450316242, 1.000000000000000000),
 ( 1.000000000000000000, 0.9152888060719367447, 1.000000000000000000) ) ) 
 REPRESENTATION_ITEM ( '' )  SURFACE ( )  );
#65306=DIRECTION ( 'NONE',  ( 1.000000000000000000, 0.000000000000000000, -1.020425574104004196E-15 ) ) ;
#65534=DIRECTION ( 'NONE',  ( 0.000000000000000000, -1.000000000000000000, 0.000000000000000000 ) ) ;
#65610=PLANE ( 'NONE',  #130392 ) ;
#65827=CARTESIAN_POINT ( 'NONE',  ( 12.84233041328156766, 9.410538608540024441, -48.93268799714088146 ) ) ;
#66180=CIRCLE ( 'NONE', #99470, 0.1000000000000001305 ) ;
#66527=DIRECTION ( 'NONE',  ( 0.000000000000000000, 0.000000000000000000, -1.000000000000000000 ) ) ;
#66594=ORIENTED_EDGE ( 'NONE', *, *, #257406, .F. ) ;
#66611=CARTESIAN_POINT ( 'NONE',  ( -16.89208623190940273, 9.951577948986638944, -54.35527220321827002 ) ) ;
#67065=CIRCLE ( 'NONE', #46201, 0.1000000000000028644 ) ;
#67109=CARTESIAN_POINT ( 'NONE',  ( -12.84409460144754433, 9.410682294279110849, -48.93114344194827936 ) ) ;
#67150=ORIENTED_EDGE ( 'NONE', *, *, #223855, .F. ) ;
#67155=ADVANCED_FACE ( 'NONE', ( #150372 ), #147800, .F. ) ;
#67166=VERTEX_POINT ( 'NONE', #13425 ) ;
#67241=ORIENTED_EDGE ( 'NONE', *, *, #164623, .T. ) ;
#67348=CARTESIAN_POINT ( 'NONE',  ( 12.25000000000000000, 9.850000000011137402, -50.24999999999999289 ) ) ;
#67605=EDGE_CURVE ( 'NONE', #145382, #137027, #7154, .T. ) ;
#68068=ORIENTED_EDGE ( 'NONE', *, *, #25286, .T. ) ;
#68118=EDGE_CURVE ( 'NONE', #91552, #196832, #190548, .T. ) ;
#68122=CARTESIAN_POINT ( 'NONE',  ( 20.73486653747088937, 7.750000000011182166, -42.75000000000000000 ) ) ;
#68207=CARTESIAN_POINT ( 'NONE',  ( -16.87998658237740912, 9.950000000011138823, -54.13636043226178884 ) ) ;
#68274=CARTESIAN_POINT ( 'NONE',  ( 15.74999999999999645, 9.850000000011137402, -50.24999999999999289 ) ) ;
#68411=AXIS2_PLACEMENT_3D ( 'NONE', #225495, #245088, #186417 ) ;
#68460=AXIS2_PLACEMENT_3D ( 'NONE', #105798, #180246, #45856 ) ;
#68493=CARTESIAN_POINT ( 'NONE',  ( -16.86379686415369861, 9.975217759264314310, -46.06661011090972124 ) ) ;
#68506=CARTESIAN_POINT ( 'NONE',  ( -17.11825945287482753, 9.950000000011138823, -46.25000000000000711 ) ) ;
#68602=ADVANCED_FACE ( 'NONE', ( #229358 ), #29083, .T. ) ;
#68611=DIRECTION ( 'NONE',  ( 1.000000000000000000, 0.000000000000000000, 0.000000000000000000 ) ) ;
#68712=ORIENTED_EDGE ( 'NONE', *, *, #107060, .T. ) ;
#69322=VECTOR ( 'NONE', #235533, 1000.000000000000000 ) ;
#69561=DIRECTION ( 'NONE',  ( -1.073024830501117725E-15, 0.000000000000000000, -1.000000000000000000 ) ) ;
#69571=CARTESIAN_POINT ( 'NONE',  ( -21.65000000000000213, 9.950000000011138823, -46.25000000000000711 ) ) ;
#69758=CARTESIAN_POINT ( 'NONE',  ( -18.40000000000000213, 11.47316190337364183, -54.39142135623731633 ) ) ;
#69790=CARTESIAN_POINT ( 'NONE',  ( -16.87368910959167678, 9.961273816702552963, -46.11249309664059837 ) ) ;
#69936=CARTESIAN_POINT ( 'NONE',  ( -20.65000000000000568, 7.250000000011138646, -54.35000000000000142 ) ) ;
#70162=DIRECTION ( 'NONE',  ( 0.000000000000000000, 0.000000000000000000, -1.000000000000000000 ) ) ;
#70461=ADVANCED_FACE ( 'NONE', ( #107523 ), #201483, .F. ) ;
#70528=DIRECTION ( 'NONE',  ( 0.000000000000000000, -1.000000000000000000, 0.000000000000000000 ) ) ;
#71372=VERTEX_POINT ( 'NONE', #119417 ) ;
#71595=ORIENTED_EDGE ( 'NONE', *, *, #141471, .F. ) ;
#71631=AXIS2_PLACEMENT_3D ( 'NONE', #140741, #23398, #238554 ) ;
#71763=CARTESIAN_POINT ( 'NONE',  ( -16.85718274719427967, 9.976142314632875596, -54.43665366781746684 ) ) ;
#71767=DIRECTION ( 'NONE',  ( 1.000000000000000000, 0.000000000000000000, 0.000000000000000000 ) ) ;
#71970=ADVANCED_FACE ( 'NONE', ( #148960 ), #227185, .T. ) ;
#72060=DIRECTION ( 'NONE',  ( -0.000000000000000000, -0.000000000000000000, -1.000000000000000000 ) ) ;
#72071=CARTESIAN_POINT ( 'NONE',  ( -16.84981964351500849, 9.917318234109957942, -54.13039838598031395 ) ) ;
#72341=ADVANCED_FACE ( 'NONE', ( #173053 ), #208297, .F. ) ;
#72524=EDGE_CURVE ( 'NONE', #26818, #114870, #239404, .T. ) ;
#72598=LINE ( 'NONE', #191269, #189367 ) ;
#72744=CARTESIAN_POINT ( 'NONE',  ( -16.93230518875208190, 10.00075036143099894, -46.07577834810150108 ) ) ;
#73099=LINE ( 'NONE', #250405, #23965 ) ;
#73430=FACE_OUTER_BOUND ( 'NONE', #183677, .T. ) ;
#73437=CARTESIAN_POINT ( 'NONE',  ( 17.74533788810829904, 10.81849979148194940, -56.68637732505243321 ) ) ;
#73622=VERTEX_POINT ( 'NONE', #22018 ) ;
#73653=CARTESIAN_POINT ( 'NONE',  ( 18.39999999999998082, 11.47316190337362585, -42.75000000000000000 ) ) ;
#74050=DIRECTION ( 'NONE',  ( -1.000000000000000000, 0.000000000000000000, 0.000000000000000000 ) ) ;
#74133=ADVANCED_FACE ( 'NONE', ( #222108 ), #111122, .F. ) ;
#74225=CARTESIAN_POINT ( 'NONE',  ( -16.87683809663752399, 9.850000000011144508, -53.59763598180369826 ) ) ;
#74530=CARTESIAN_POINT ( 'NONE',  ( -16.90128866880176162, 9.953795777214113016, -54.36267618338864338 ) ) ;
#74588=ORIENTED_EDGE ( 'NONE', *, *, #25286, .F. ) ;
#74729=CARTESIAN_POINT ( 'NONE',  ( 12.42718393586866732, 9.370655051134640701, -51.02582325598088175 ) ) ;
#75191=DIRECTION ( 'NONE',  ( -0.000000000000000000, -0.000000000000000000, -1.000000000000000000 ) ) ;
#75496=CARTESIAN_POINT ( 'NONE',  ( -16.95709691156394427, 9.950000000011280932, -46.16005756250920911 ) ) ;
#75512=ORIENTED_EDGE ( 'NONE', *, *, #194657, .T. ) ;
#75789=CARTESIAN_POINT ( 'NONE',  ( -16.81453563122427397, 9.939100205448108127, -54.28825866064529748 ) ) ;
#75937=CARTESIAN_POINT ( 'NONE',  ( -13.11924609551135035, 9.431689550535260480, -51.77929003223608362 ) ) ;
#75972=CARTESIAN_POINT ( 'NONE',  ( 12.26145404764308289, 9.351413679112543065, -50.48034356754896379 ) ) ;
#76146=CARTESIAN_POINT ( 'NONE',  ( -16.87435696428308063, 9.950002462943377424, -46.14999176516656831 ) ) ;
#76170=ADVANCED_BREP_SHAPE_REPRESENTATION ( '', ( #25658, #2425 ), #32042 ) ;
#76659=UNCERTAINTY_MEASURE_WITH_UNIT (LENGTH_MEASURE( 1.000000000000000082E-05 ), #152956, 'distance_accuracy_value', 'NONE');
#76673=ORIENTED_EDGE ( 'NONE', *, *, #29484, .T. ) ;
#76980=CARTESIAN_POINT ( 'NONE',  ( -18.40000000000000213, 11.75000000001113953, -54.35000000000000142 ) ) ;
#77204=VECTOR ( 'NONE', #36254, 1000.000000000000000 ) ;
#77419=CARTESIAN_POINT ( 'NONE',  ( -18.40000000000000213, 11.33174054713631662, -46.15000000000000568 ) ) ;
#77456=DIRECTION ( 'NONE',  ( -0.000000000000000000, 1.000000000000000000, 0.000000000000000000 ) ) ;
#77667=VECTOR ( 'NONE', #29010, 1000.000000000000000 ) ;
#77706=ORIENTED_EDGE ( 'NONE', *, *, #211308, .F. ) ;
#77724=EDGE_LOOP ( 'NONE', ( #137250, #44738, #192469 ) ) ;
#77777=CARTESIAN_POINT ( 'NONE',  ( -16.83558968593870375, 9.950000000011137047, -46.16230518761685175 ) ) ;
#77877=LINE ( 'NONE', #177025, #147665 ) ;
#78235=ADVANCED_FACE ( 'NONE', ( #206413 ), #65610, .F. ) ;
#78481=CARTESIAN_POINT ( 'NONE',  ( -15.06720934482787833, 9.417690691074259490, -51.64160069676458420 ) ) ;
#78643=ORIENTED_EDGE ( 'NONE', *, *, #24997, .T. ) ;
#78644=CARTESIAN_POINT ( 'NONE',  ( -16.94225986326250677, 9.950000000011138823, -46.44671937560789132 ) ) ;
#79050=CARTESIAN_POINT ( 'NONE',  ( -16.77180007708461318, 9.950000000011137047, -46.13561411895483388 ) ) ;
#79138=CARTESIAN_POINT ( 'NONE',  ( -17.11825945287482753, 9.950000000011138823, -46.25000000000000711 ) ) ;
#79306=DIRECTION ( 'NONE',  ( 0.000000000000000000, -0.000000000000000000, -1.000000000000000000 ) ) ;
#79438=CARTESIAN_POINT ( 'NONE',  ( -18.41431012584569160, 11.48747202921933130, -57.77323601310166623 ) ) ;
#79469=FACE_OUTER_BOUND ( 'NONE', #104160, .T. ) ;
#79769=ORIENTED_EDGE ( 'NONE', *, *, #246193, .T. ) ;
#79770=VECTOR ( 'NONE', #190494, 1000.000000000000000 ) ;
#79970=EDGE_CURVE ( 'NONE', #230747, #53148, #73099, .T. ) ;
#80549=CARTESIAN_POINT ( 'NONE',  ( -16.93211319090181988, 9.999986781168624717, -54.42250549927307191 ) ) ;
#80721=DIRECTION ( 'NONE',  ( -1.000000000000000000, 0.000000000000000000, 0.000000000000000000 ) ) ;
#80810=CYLINDRICAL_SURFACE ( 'NONE', #209887, 1.749999999999999778 ) ;
#81101=DIRECTION ( 'NONE',  ( 1.000000000000000000, 0.000000000000000000, 1.073024830501117725E-15 ) ) ;
#81107=CARTESIAN_POINT ( 'NONE',  ( -16.78805706634180339, 9.948252493082335945, -54.34415320803185523 ) ) ;
#81125=CARTESIAN_POINT ( 'NONE',  ( 18.39999999999999503, 11.47316190337363828, -54.35000000000000142 ) ) ;
#81226=CARTESIAN_POINT ( 'NONE',  ( -16.97683809663752186, 9.850000000011137402, -46.90236401819648648 ) ) ;
#81330=LINE ( 'NONE', #180476, #111928 ) ;
#81430=CARTESIAN_POINT ( 'NONE',  ( -16.87304349924914604, 9.961745077968330975, -54.38906667504524961 ) ) ;
#81560=CARTESIAN_POINT ( 'NONE',  ( -16.79139129368504157, 9.944944162472829419, -46.17024463282581337 ) ) ;
#81675=AXIS2_PLACEMENT_3D ( 'NONE', #223977, #200573, #239711 ) ;
#82369=CARTESIAN_POINT ( 'NONE',  ( 18.39999999999999503, 11.75000000001113953, -54.35000000000000142 ) ) ;
#82561=CARTESIAN_POINT ( 'NONE',  ( -17.11825945287481332, 9.950000000011138823, -54.25000000000000711 ) ) ;
#82601=EDGE_CURVE ( 'NONE', #73622, #155471, #92830, .T. ) ;
#82690=EDGE_CURVE ( 'NONE', #141210, #43598, #234791, .T. ) ;
#82820=PLANE ( 'NONE',  #144630 ) ;
#82880=DIRECTION ( 'NONE',  ( 1.186688945009010077E-16, -1.000000000000000000, -0.000000000000000000 ) ) ;
#82977=CARTESIAN_POINT ( 'NONE',  ( 15.51872946208854565, 9.376580978055097049, -51.12694624701192225 ) ) ;
#83266=CARTESIAN_POINT ( 'NONE',  ( -16.93658623642902938, 9.980381671668283161, -46.11190272912921273 ) ) ;
#83794=CARTESIAN_POINT ( 'NONE',  ( -18.34804628011471195, 11.47316190337353525, -42.75000000000000000 ) ) ;
#83856=CARTESIAN_POINT ( 'NONE',  ( -21.65000000000000213, 7.250000000011138646, -46.15000000000000568 ) ) ;
#83954=CARTESIAN_POINT ( 'NONE',  ( -12.25000000000000178, 9.350000000011139178, -50.25000000000000000 ) ) ;
#84049=CARTESIAN_POINT ( 'NONE',  ( -14.77738660682464022, 9.436552840015577814, -48.67795547276032408 ) ) ;
#84143=ORIENTED_EDGE ( 'NONE', *, *, #202515, .F. ) ;
#84198=AXIS2_PLACEMENT_3D ( 'NONE', #104291, #183849, #24812 ) ;
#84283=CARTESIAN_POINT ( 'NONE',  ( -21.64999999999999858, 9.350000000011133849, -46.15000000000000568 ) ) ;
#84635=CARTESIAN_POINT ( 'NONE',  ( -18.40000000000000213, 11.33174054713631662, -46.15000000000000568 ) ) ;
#84734=EDGE_CURVE ( 'NONE', #47133, #52893, #59587, .T. ) ;
#84917=CARTESIAN_POINT ( 'NONE',  ( -33.72168855820452649, 11.47316190337362940, -57.75000000000000711 ) ) ;
#84939=ORIENTED_EDGE ( 'NONE', *, *, #95352, .T. ) ;
#84964=CARTESIAN_POINT ( 'NONE',  ( -17.71734398241073905, 10.84235722847571814, -43.77486174699441079 ) ) ;
#85046=CARTESIAN_POINT ( 'NONE',  ( -16.90137573187933384, 9.950000000011135270, -46.28841742409689175 ) ) ;
#85127=( BOUNDED_SURFACE ( )  B_SPLINE_SURFACE ( 3, 2, ( 
 ( #256758, #100278, #37790 ),
 ( #118607, #18205, #178594 ),
 ( #242374, #101553, #136862 ),
 ( #258050, #79438, #238532 ) ),
 .UNSPECIFIED., .F., .F., .F. ) 
 B_SPLINE_SURFACE_WITH_KNOTS ( ( 4, 4 ),
 ( 3, 3 ),
 ( 0.3000847527772381729, 0.5552748953338751958 ),
 ( 0.000000000000000000, 1.000000000000000000 ),
 .UNSPECIFIED. ) 
 GEOMETRIC_REPRESENTATION_ITEM ( )  RATIONAL_B_SPLINE_SURFACE ( (
 ( 1.000000000000000000, 0.9152888060719349683, 1.000000000000000000),
 ( 1.000000000000000000, 0.9104333467450302919, 1.000000000000000000),
 ( 1.000000000000000000, 0.9035312726220549040, 1.000000000000000000),
 ( 1.000000000000000000, 0.8946697475932153809, 1.000000000000000000) ) ) 
 REPRESENTATION_ITEM ( '' )  SURFACE ( )  );
#85128=CARTESIAN_POINT ( 'NONE',  ( -16.87331047859649757, 9.950000000011138823, -54.35000000000000142 ) ) ;
#85204=SURFACE_STYLE_USAGE ( .BOTH. , #26575 ) ;
#85422=VECTOR ( 'NONE', #109029, 1000.000000000000000 ) ;
#85569=CARTESIAN_POINT ( 'NONE',  ( -16.81095280782811230, 9.950000000011138823, -46.14999999999913172 ) ) ;
#85740=ADVANCED_FACE ( 'NONE', ( #144128 ), #243238, .F. ) ;
#85901=ORIENTED_EDGE ( 'NONE', *, *, #121818, .F. ) ;
#85933=FACE_OUTER_BOUND ( 'NONE', #145220, .T. ) ;
#85999=CYLINDRICAL_SURFACE ( 'NONE', #84198, 0.1000000000000028644 ) ;
#86106=ORIENTED_EDGE ( 'NONE', *, *, #250264, .T. ) ;
#86282=DIRECTION ( 'NONE',  ( -0.7071067811865456854, 0.7071067811865493491, 0.000000000000000000 ) ) ;
#86331=CARTESIAN_POINT ( 'NONE',  ( -16.89020380669786547, 9.950000000011135270, -46.25741114811057741 ) ) ;
#86509=CARTESIAN_POINT ( 'NONE',  ( -33.72168855820451938, 9.950000000011156587, -46.14999999999994884 ) ) ;
#86636=CARTESIAN_POINT ( 'NONE',  ( -13.43673303185029688, 9.446648990640015953, -48.58916329592318561 ) ) ;
#86648=CARTESIAN_POINT ( 'NONE',  ( 15.39793903038207823, 9.389686005666812108, -49.17284350635129897 ) ) ;
#86703=CARTESIAN_POINT ( 'NONE',  ( -16.85312841634287651, 9.913606177331356406, -46.39717313329252590 ) ) ;
#86828=ORIENTED_EDGE ( 'NONE', *, *, #202515, .T. ) ;
#87121=DIRECTION ( 'NONE',  ( 1.000000000000000000, 0.000000000000000000, -0.000000000000000000 ) ) ;
#87132=DIRECTION ( 'NONE',  ( -1.000000000000000000, 0.000000000000000000, 0.000000000000000000 ) ) ;
#87215=VECTOR ( 'NONE', #63744, 1000.000000000000000 ) ;
#87302=CARTESIAN_POINT ( 'NONE',  ( 23.24999999999999645, 11.75000000001113953, -42.75000000000000000 ) ) ;
#87346=DIRECTION ( 'NONE',  ( -1.000000000000000000, 0.000000000000000000, 0.000000000000000000 ) ) ;
#87611=ORIENTED_EDGE ( 'NONE', *, *, #118019, .T. ) ;
#87733=CARTESIAN_POINT ( 'NONE',  ( 22.88900146558018989, 8.703904791123973084, -42.75000000000000000 ) ) ;
#87751=LINE ( 'NONE', #167334, #131143 ) ;
#87937=CARTESIAN_POINT ( 'NONE',  ( 14.45204356427542081, 9.450668889178686527, -48.55554649020735525 ) ) ;
#88032=EDGE_CURVE ( 'NONE', #225035, #149877, #102666, .T. ) ;
#88530=DIRECTION ( 'NONE',  ( 1.000000000000000000, 0.000000000000000000, 0.000000000000000000 ) ) ;
#88800=ORIENTED_EDGE ( 'NONE', *, *, #67605, .T. ) ;
#89020=DIRECTION ( 'NONE',  ( 0.000000000000000000, 0.000000000000000000, 1.000000000000000000 ) ) ;
#89039=CARTESIAN_POINT ( 'NONE',  ( -16.80891096016331687, 9.950000000011137047, -54.36766280726798328 ) ) ;
#89327=CARTESIAN_POINT ( 'NONE',  ( -17.01473183483382101, 9.950000000011138823, -46.25000000000000000 ) ) ;
#89461=ADVANCED_FACE ( 'NONE', ( #139140 ), #217409, .T. ) ;
#89764=LINE ( 'NONE', #96178, #149487 ) ;
#90226=ADVANCED_FACE ( 'NONE', ( #85933 ), #80810, .F. ) ;
#90311=VERTEX_POINT ( 'NONE', #220358 ) ;
#90317=CARTESIAN_POINT ( 'NONE',  ( -16.93710578446422588, 9.950000000011137047, -54.08119601620066419 ) ) ;
#90365=( NAMED_UNIT ( * ) PLANE_ANGLE_UNIT ( ) SI_UNIT ( $, .RADIAN. ) );
#90653=CARTESIAN_POINT ( 'NONE',  ( -18.38817693311004575, 11.48149151591092476, -57.75000000000000000 ) ) ;
#90980=CARTESIAN_POINT ( 'NONE',  ( -16.93339986808596365, 10.00510392857707664, -46.06599367181285487 ) ) ;
#91001=ADVANCED_FACE ( 'NONE', ( #140167 ), #98444, .T. ) ;
#91208=CIRCLE ( 'NONE', #241069, 14.30833333333333890 ) ;
#91247=ORIENTED_EDGE ( 'NONE', *, *, #227533, .T. ) ;
#91364=SHAPE_DEFINITION_REPRESENTATION ( #124202, #223420 ) ;
#91436=CARTESIAN_POINT ( 'NONE',  ( -16.94107738177415712, 10.01423928514777728, -46.04999999999999716 ) ) ;
#91552=VERTEX_POINT ( 'NONE', #196652 ) ;
#91739=ORIENTED_EDGE ( 'NONE', *, *, #109981, .T. ) ;
#91741=ADVANCED_FACE ( 'NONE', ( #101355 ), #3587, .F. ) ;
#91865=CARTESIAN_POINT ( 'NONE',  ( -16.88219499860498019, 9.950206425438743452, -46.14930969010730166 ) ) ;
#91946=CARTESIAN_POINT ( 'NONE',  ( -18.36973785203556275, 11.47550320049537476, -57.75000000000000000 ) ) ;
#92092=EDGE_CURVE ( 'NONE', #136044, #22095, #152570, .T. ) ;
#92110=VECTOR ( 'NONE', #175217, 1000.000000000000000 ) ;
#92194=ORIENTED_EDGE ( 'NONE', *, *, #121818, .T. ) ;
#92259=CARTESIAN_POINT ( 'NONE',  ( -16.93658211146646408, 9.994108662352344297, -46.09570493004432734 ) ) ;
#92635=ORIENTED_EDGE ( 'NONE', *, *, #23480, .T. ) ;
#92662=EDGE_CURVE ( 'NONE', #152757, #228728, #145052, .T. ) ;
#92830=( BOUNDED_CURVE ( )  B_SPLINE_CURVE ( 3, ( #91436, #229659, #9321, #50985 ),
 .UNSPECIFIED., .F., .F. ) 
 B_SPLINE_CURVE_WITH_KNOTS ( ( 4, 4 ),
 ( 0.3000847527772381729, 0.5497968875596822569 ),
 .UNSPECIFIED. ) 
 CURVE ( )  GEOMETRIC_REPRESENTATION_ITEM ( )  RATIONAL_B_SPLINE_CURVE ( ( 1.000000000000000000, 0.9948104011409419911, 0.9948104011409419911, 1.000000000000000000 ) ) 
 REPRESENTATION_ITEM ( '' )  );
#92953=DIRECTION ( 'NONE',  ( -1.000000000000000000, 0.000000000000000000, 1.073024830501117725E-15 ) ) ;
#93043=VECTOR ( 'NONE', #167842, 999.9999999999998863 ) ;
#93652=ORIENTED_EDGE ( 'NONE', *, *, #252956, .T. ) ;
#93739=CARTESIAN_POINT ( 'NONE',  ( -23.25000000000000355, 11.75000000001113953, -46.15000000000000568 ) ) ;
#93870=PLANE ( 'NONE',  #218789 ) ;
#94052=EDGE_CURVE ( 'NONE', #9728, #197944, #178503, .T. ) ;
#94198=CARTESIAN_POINT ( 'NONE',  ( -12.25000000000000000, 9.350000000011133849, -50.36574316727391221 ) ) ;
#94240=CARTESIAN_POINT ( 'NONE',  ( 13.54577453029516221, 9.450602096099677496, -51.94389596309667922 ) ) ;
#94268=ORIENTED_EDGE ( 'NONE', *, *, #231318, .T. ) ;
#94424=CARTESIAN_POINT ( 'NONE',  ( -16.87487986503753845, 9.950007555096753720, -46.14997473968674058 ) ) ;
#94700=DIRECTION ( 'NONE',  ( -1.000000000000000000, 0.000000000000000000, 0.000000000000000000 ) ) ;
#94720=CARTESIAN_POINT ( 'NONE',  ( 23.24999999999999645, 11.75000000001113953, -42.75000000000000000 ) ) ;
#95085=( BOUNDED_SURFACE ( )  B_SPLINE_SURFACE ( 3, 2, ( 
 ( #16799, #192861, #177169 ),
 ( #254088, #96292, #155036 ),
 ( #213691, #75496, #196686 ),
 ( #234537, #217525, #38922 ) ),
 .UNSPECIFIED., .F., .F., .F. ) 
 B_SPLINE_SURFACE_WITH_KNOTS ( ( 4, 4 ),
 ( 3, 3 ),
 ( 4.712388980384689674, 5.765869716888459173 ),
 ( 0.000000000000000000, 1.000000000000000000 ),
 .UNSPECIFIED. ) 
 GEOMETRIC_REPRESENTATION_ITEM ( )  RATIONAL_B_SPLINE_SURFACE ( (
 ( 1.000000000000000000, 0.7071067811865229258, 1.000000000000000000),
 ( 1.000000000000000000, 0.7953136715913396992, 1.000000000000000000),
 ( 1.000000000000000000, 0.8646876308615339957, 1.000000000000000000),
 ( 1.000000000000000000, 0.8984936768950558816, 1.000000000000000000) ) ) 
 REPRESENTATION_ITEM ( '' )  SURFACE ( )  );
#95100=DIRECTION ( 'NONE',  ( 1.020425574104004196E-15, 1.210927747993693964E-31, 1.000000000000000000 ) ) ;
#95342=FACE_OUTER_BOUND ( 'NONE', #247896, .T. ) ;
#95352=EDGE_CURVE ( 'NONE', #40566, #132925, #127947, .T. ) ;
#95527=CARTESIAN_POINT ( 'NONE',  ( 12.68104795156994768, 9.396533993965078935, -51.40593977917330193 ) ) ;
#95587=ORIENTED_EDGE ( 'NONE', *, *, #171932, .T. ) ;
#95615=ORIENTED_EDGE ( 'NONE', *, *, #141912, .T. ) ;
#95706=CARTESIAN_POINT ( 'NONE',  ( -16.89060415895971090, 9.951220762813354881, -46.14592022427046203 ) ) ;
#95727=B_SPLINE_CURVE_WITH_KNOTS ( 'NONE', 3,
 ( #205375, #142825, #81560, #101101, #146675, #41217, #43755, #185828, #7176, #86703, #120754, #2041, #240668, #30637 ),
 .UNSPECIFIED., .F., .F.,
 ( 4, 2, 2, 2, 2, 2, 4 ),
 ( 0.000000000000000000, 2.389617747644075618E-05, 4.779235495288151236E-05, 9.558470990574922824E-05, 0.0001911694198114619731, 0.0003823388396229078457, 0.0007646776792457995369 ),
 .UNSPECIFIED. ) ;
#95731=CARTESIAN_POINT ( 'NONE',  ( -17.05016517656233432, 9.950000000010200907, -54.32730200400028053 ) ) ;
#96061=CARTESIAN_POINT ( 'NONE',  ( -16.80621392010913340, 9.942202577518862938, -46.18959196541719336 ) ) ;
#96077=EDGE_CURVE ( 'NONE', #109277, #227367, #143007, .T. ) ;
#96178=CARTESIAN_POINT ( 'NONE',  ( 20.27550659511088682, 9.216043722520002035, -42.75000000000000000 ) ) ;
#96229=ORIENTED_EDGE ( 'NONE', *, *, #109981, .F. ) ;
#96292=CARTESIAN_POINT ( 'NONE',  ( -17.05016517656101627, 9.950000000012078516, -46.17269799600016000 ) ) ;
#96447=AXIS2_PLACEMENT_3D ( 'NONE', #128164, #224674, #126877 ) ;
#96463=CARTESIAN_POINT ( 'NONE',  ( 23.24999999999999645, 5.650000000011139001, -54.34999999999999432 ) ) ;
#96497=DIRECTION ( 'NONE',  ( -1.000000000000000000, 0.000000000000000000, 0.000000000000000000 ) ) ;
#96564=ORIENTED_EDGE ( 'NONE', *, *, #815, .F. ) ;
#96670=DIRECTION ( 'NONE',  ( 1.020425574104004196E-15, 1.210927747993693964E-31, -1.000000000000000000 ) ) ;
#96745=CARTESIAN_POINT ( 'NONE',  ( -14.56336952470180179, 9.446645344706404046, -51.91080645610022515 ) ) ;
#97246=CARTESIAN_POINT ( 'NONE',  ( 18.39999999999999503, 11.75000000001113953, -46.15000000000000568 ) ) ;
#97258=VERTEX_POINT ( 'NONE', #102091 ) ;
#97321=CARTESIAN_POINT ( 'NONE',  ( -16.92280123533723213, 9.950000000011137047, -46.35063231408512507 ) ) ;
#98153=DIRECTION ( 'NONE',  ( -0.5932847527679310229, 0.8049926720990042694, -6.366092712777067056E-16 ) ) ;
#98185=CARTESIAN_POINT ( 'NONE',  ( -16.97048326478264713, 9.950000000011137047, -46.64110688012716821 ) ) ;
#98343=FACE_OUTER_BOUND ( 'NONE', #21502, .T. ) ;
#98351=CARTESIAN_POINT ( 'NONE',  ( -21.65000000000000213, 7.250000000011139534, -46.15000000000000568 ) ) ;
#98444=PLANE ( 'NONE',  #114381 ) ;
#98598=CARTESIAN_POINT ( 'NONE',  ( -16.97683810757273193, 9.950000000011137047, -46.76357671246011449 ) ) ;
#98608=( GEOMETRIC_REPRESENTATION_CONTEXT ( 3 ) GLOBAL_UNCERTAINTY_ASSIGNED_CONTEXT ( ( #102614 ) ) GLOBAL_UNIT_ASSIGNED_CONTEXT ( ( #58915, #177649, #248 ) ) REPRESENTATION_CONTEXT ( 'NONE', 'WORKASPACE' ) );
#98663=FACE_OUTER_BOUND ( 'NONE', #243351, .T. ) ;
#98664=EDGE_CURVE ( 'NONE', #165658, #203380, #39364, .T. ) ;
#98676=CARTESIAN_POINT ( 'NONE',  ( -16.92973740335363075, 9.992503814478597590, -46.09394096479768166 ) ) ;
#98813=VERTEX_POINT ( 'NONE', #201263 ) ;
#98842=ORIENTED_EDGE ( 'NONE', *, *, #149409, .F. ) ;
#98883=CARTESIAN_POINT ( 'NONE',  ( -20.65000000000000568, 7.250000000011138646, -54.35000000000000142 ) ) ;
#98894=LINE ( 'NONE', #212476, #189539 ) ;
#98896=ADVANCED_FACE ( 'NONE', ( #5609 ), #225936, .F. ) ;
#99008=AXIS2_PLACEMENT_3D ( 'NONE', #57835, #151853, #253479 ) ;
#99097=ORIENTED_EDGE ( 'NONE', *, *, #183227, .T. ) ;
#99126=DIRECTION ( 'NONE',  ( -0.000000000000000000, -0.000000000000000000, -1.000000000000000000 ) ) ;
#99148=ORIENTED_EDGE ( 'NONE', *, *, #24475, .F. ) ;
#99280=PLANE ( 'NONE',  #199984 ) ;
#99318=CARTESIAN_POINT ( 'NONE',  ( -15.57281606413133623, 9.370655051134644253, -51.02582325598089596 ) ) ;
#99330=ORIENTED_EDGE ( 'NONE', *, *, #216208, .F. ) ;
#99470=AXIS2_PLACEMENT_3D ( 'NONE', #207381, #245219, #30041 ) ;
#99642=DIRECTION ( 'NONE',  ( -0.000000000000000000, -0.000000000000000000, -1.000000000000000000 ) ) ;
#99857=ORIENTED_EDGE ( 'NONE', *, *, #27128, .T. ) ;
#100032=ORIENTED_EDGE ( 'NONE', *, *, #190918, .F. ) ;
#100166=VERTEX_POINT ( 'NONE', #206451 ) ;
#100253=EDGE_CURVE ( 'NONE', #67166, #225035, #44812, .T. ) ;
#100278=CARTESIAN_POINT ( 'NONE',  ( -16.91256925476569606, 9.985731158139328656, -54.46764248900526439 ) ) ;
#100421=ORIENTED_EDGE ( 'NONE', *, *, #130925, .F. ) ;
#100491=ORIENTED_EDGE ( 'NONE', *, *, #55589, .T. ) ;
#100652=CARTESIAN_POINT ( 'NONE',  ( -16.77779411440718604, 9.946101447118758543, -54.33694258299546220 ) ) ;
#100905=FILL_AREA_STYLE ('',( #64403 ) ) ;
#101082=DIRECTION ( 'NONE',  ( 0.000000000000000000, 0.000000000000000000, 1.000000000000000000 ) ) ;
#101101=CARTESIAN_POINT ( 'NONE',  ( -16.80100426158790228, 9.943150520407293413, -46.18294575283405834 ) ) ;
#101355=FACE_OUTER_BOUND ( 'NONE', #3108, .T. ) ;
#101359=ORIENTED_EDGE ( 'NONE', *, *, #149482, .F. ) ;
#101553=CARTESIAN_POINT ( 'NONE',  ( -17.78241384942201364, 10.85557575279799991, -56.75096232754270886 ) ) ;
#101657=CARTESIAN_POINT ( 'NONE',  ( 18.39999999999999503, 11.75000000001113953, -46.15000000000000568 ) ) ;
#101968=VECTOR ( 'NONE', #98153, 1000.000000000000000 ) ;
#102091=CARTESIAN_POINT ( 'NONE',  ( -16.77683809663752257, 9.945835743215303282, -54.33605098089579855 ) ) ;
#102297=EDGE_LOOP ( 'NONE', ( #149703, #1665, #195088, #250865 ) ) ;
#102345=CARTESIAN_POINT ( 'NONE',  ( -12.29659703204452370, 9.355888454513703323, -49.78864289677800770 ) ) ;
#102487=AXIS2_PLACEMENT_3D ( 'NONE', #224819, #167458, #183152 ) ;
#102542=CARTESIAN_POINT ( 'NONE',  ( 20.09999999999999787, 9.750000000011137757, -54.34999999999999432 ) ) ;
#102613=DIRECTION ( 'NONE',  ( 1.186688945009010077E-16, -1.000000000000000000, -0.000000000000000000 ) ) ;
#102614=UNCERTAINTY_MEASURE_WITH_UNIT (LENGTH_MEASURE( 1.000000000000000082E-05 ), #58915, 'distance_accuracy_value', 'NONE');
#102666=CIRCLE ( 'NONE', #223492, 0.5000000000000004441 ) ;
#102761=VERTEX_POINT ( 'NONE', #193122 ) ;
#102874=CYLINDRICAL_SURFACE ( 'NONE', #71631, 0.9000000000000014655 ) ;
#102959=DIRECTION ( 'NONE',  ( -1.000000000000000000, -0.000000000000000000, 1.073024830501117725E-15 ) ) ;
#103414=CARTESIAN_POINT ( 'NONE',  ( 20.27550659511089037, 9.216043722520002035, -46.15000000000000568 ) ) ;
#103724=ORIENTED_EDGE ( 'NONE', *, *, #229472, .T. ) ;
#103774=EDGE_LOOP ( 'NONE', ( #251594, #85901, #86106, #93652 ) ) ;
#103951=CARTESIAN_POINT ( 'NONE',  ( 18.39999999999999503, 5.650000000011139001, -57.75000000000000711 ) ) ;
#104032=ORIENTED_EDGE ( 'NONE', *, *, #179562, .T. ) ;
#104122=CARTESIAN_POINT ( 'NONE',  ( -16.94333152886235894, 9.990342011461638805, -46.10796846894559309 ) ) ;
#104147=EDGE_CURVE ( 'NONE', #129130, #129914, #154729, .T. ) ;
#104160=EDGE_LOOP ( 'NONE', ( #164808, #220294, #5289, #96564 ) ) ;
#104291=CARTESIAN_POINT ( 'NONE',  ( -23.25000000000000355, 10.05000000001113847, -54.25000000000000711 ) ) ;
#104529=CARTESIAN_POINT ( 'NONE',  ( -16.87036670365549895, 9.989418819312803066, -46.02043988269794994 ) ) ;
#104588=ORIENTED_EDGE ( 'NONE', *, *, #245717, .T. ) ;
#104591=VERTEX_POINT ( 'NONE', #213081 ) ;
#104838=CARTESIAN_POINT ( 'NONE',  ( -16.86420534634261514, 9.970615445602874161, -54.41833654923738095 ) ) ;
#104936=ADVANCED_FACE ( 'NONE', ( #152846 ), #52406, .F. ) ;
#105064=DIRECTION ( 'NONE',  ( -0.000000000000000000, -0.000000000000000000, -1.000000000000000000 ) ) ;
#105073=VERTEX_POINT ( 'NONE', #199660 ) ;
#105080=VECTOR ( 'NONE', #190079, 1000.000000000000000 ) ;
#105307=ORIENTED_EDGE ( 'NONE', *, *, #203874, .T. ) ;
#105309=ORIENTED_EDGE ( 'NONE', *, *, #159394, .T. ) ;
#105538=PLANE ( 'NONE',  #68411 ) ;
#105697=ORIENTED_EDGE ( 'NONE', *, *, #199683, .F. ) ;
#105798=CARTESIAN_POINT ( 'NONE',  ( -16.87683809663752399, 23.65833333334447985, -50.25000000000000000 ) ) ;
#105985=ORIENTED_EDGE ( 'NONE', *, *, #168028, .F. ) ;
#106045=LINE ( 'NONE', #241731, #249366 ) ;
#106052=ORIENTED_EDGE ( 'NONE', *, *, #18515, .T. ) ;
#106159=LINE ( 'NONE', #201422, #255548 ) ;
#106211=CARTESIAN_POINT ( 'NONE',  ( -15.06774609480955363, 9.417651958852161442, -48.85878739244044056 ) ) ;
#106218=CARTESIAN_POINT ( 'NONE',  ( 14.87567385445977663, 9.430764995433474240, -48.73053739475045631 ) ) ;
#106336=AXIS2_PLACEMENT_3D ( 'NONE', #187090, #42420, #142778 ) ;
#106431=CARTESIAN_POINT ( 'NONE',  ( -16.78569801330232636, 9.947933733124651567, -46.15691290534750379 ) ) ;
#106477=EDGE_LOOP ( 'NONE', ( #179558, #98842, #95615, #39748 ) ) ;
#106811=ORIENTED_EDGE ( 'NONE', *, *, #95352, .F. ) ;
#107060=EDGE_CURVE ( 'NONE', #21668, #144797, #225970, .T. ) ;
#107379=CARTESIAN_POINT ( 'NONE',  ( 14.45963434102923628, 9.451541661396666072, -51.95387549883057687 ) ) ;
#107416=CARTESIAN_POINT ( 'NONE',  ( -18.40000000000000213, 11.33174054713633261, -54.35000000000000142 ) ) ;
#107437=DIRECTION ( 'NONE',  ( 1.000000000000000000, 0.000000000000000000, 0.000000000000000000 ) ) ;
#107510=CARTESIAN_POINT ( 'NONE',  ( -12.25000000000000178, 9.350000000011139178, -50.25000000000000000 ) ) ;
#107521=CARTESIAN_POINT ( 'NONE',  ( 13.43443725621852636, 9.446557523083688679, -48.58994195434588903 ) ) ;
#107523=FACE_OUTER_BOUND ( 'NONE', #176209, .T. ) ;
#107566=DIRECTION ( 'NONE',  ( 0.7071067811865474617, 0.7071067811865474617, 0.000000000000000000 ) ) ;
#107672=DIRECTION ( 'NONE',  ( -1.073024830501117725E-15, 0.000000000000000000, 1.000000000000000000 ) ) ;
#108496=CARTESIAN_POINT ( 'NONE',  ( -16.84421487269769102, 9.950000000011137047, -46.16950212244496043 ) ) ;
#108500=CARTESIAN_POINT ( 'NONE',  ( 18.39999999999999503, 11.75000000001113953, -57.75000000000000711 ) ) ;
#108563=ORIENTED_EDGE ( 'NONE', *, *, #53876, .T. ) ;
#108874=DIRECTION ( 'NONE',  ( 0.000000000000000000, -0.000000000000000000, -1.000000000000000000 ) ) ;
#108998=DIRECTION ( 'NONE',  ( 0.000000000000000000, 0.000000000000000000, -1.000000000000000000 ) ) ;
#109029=DIRECTION ( 'NONE',  ( -1.652117596168391700E-15, -1.000000000000000000, 0.000000000000000000 ) ) ;
#109154=ORIENTED_EDGE ( 'NONE', *, *, #110923, .T. ) ;
#109277=VERTEX_POINT ( 'NONE', #111539 ) ;
#109314=DIRECTION ( 'NONE',  ( -1.000000000000000000, 0.000000000000000000, 0.000000000000000000 ) ) ;
#109432=ADVANCED_FACE ( 'NONE', ( #98343 ), #177942, .T. ) ;
#109480=FACE_OUTER_BOUND ( 'NONE', #48113, .T. ) ;
#109681=ORIENTED_EDGE ( 'NONE', *, *, #118208, .F. ) ;
#109719=EDGE_LOOP ( 'NONE', ( #160496, #175924, #29641, #11402 ) ) ;
#109817=DIRECTION ( 'NONE',  ( -1.000000000000000000, 0.000000000000000000, 0.000000000000000000 ) ) ;
#109873=CARTESIAN_POINT ( 'NONE',  ( -16.89268316805465986, 9.951721813253337601, -54.35575247854554704 ) ) ;
#109883=CARTESIAN_POINT ( 'NONE',  ( -16.83233564386402037, 9.930221796595782635, -54.22452066347574373 ) ) ;
#109957=CIRCLE ( 'NONE', #197437, 0.09999999999999939493 ) ;
#109981=EDGE_CURVE ( 'NONE', #193307, #151638, #147485, .T. ) ;
#110120=ORIENTED_EDGE ( 'NONE', *, *, #19918, .T. ) ;
#110157=ORIENTED_EDGE ( 'NONE', *, *, #189487, .F. ) ;
#110458=DIRECTION ( 'NONE',  ( 1.000000000000000000, 0.000000000000000000, -0.000000000000000000 ) ) ;
#110612=AXIS2_PLACEMENT_3D ( 'NONE', #240991, #220148, #118489 ) ;
#110684=CARTESIAN_POINT ( 'NONE',  ( 20.04999999999999716, 8.750000000011173285, -54.35000000000000142 ) ) ;
#110872=DIRECTION ( 'NONE',  ( 1.186688945009010077E-16, -1.000000000000000000, -0.000000000000000000 ) ) ;
#110923=EDGE_CURVE ( 'NONE', #231063, #222258, #49337, .T. ) ;
#111091=( BOUNDED_CURVE ( )  B_SPLINE_CURVE ( 3, ( #12399, #52768, #89327, #68506 ),
 .UNSPECIFIED., .F., .F. ) 
 B_SPLINE_CURVE_WITH_KNOTS ( ( 4, 4 ),
 ( 0.5235987755983128045, 1.570796326794896558 ),
 .UNSPECIFIED. ) 
 CURVE ( )  GEOMETRIC_REPRESENTATION_ITEM ( )  RATIONAL_B_SPLINE_CURVE ( ( 1.000000000000000000, 0.9106836025229614329, 0.9106836025229614329, 1.000000000000000000 ) ) 
 REPRESENTATION_ITEM ( '' )  );
#111122=( BOUNDED_SURFACE ( )  B_SPLINE_SURFACE ( 3, 2, ( 
 ( #145151, #224693, #46062 ),
 ( #205121, #185578, #6938 ),
 ( #10802, #210296, #129466 ),
 ( #128181, #29126, #90317 ),
 ( #72071, #68207, #31678 ),
 ( #109883, #208996, #147747 ),
 ( #169921, #30379, #48628 ),
 ( #189445, #249420, #168644 ),
 ( #9504, #248118, #89039 ),
 ( #49918, #151625, #211575 ) ),
 .UNSPECIFIED., .F., .F., .F. ) 
 B_SPLINE_SURFACE_WITH_KNOTS ( ( 4, 2, 2, 2, 4 ),
 ( 3, 3 ),
 ( 0.002161241639767248670, 0.002579950749615824400, 0.002789305304540112482, 0.002893982582002256523, 0.002998659859464400564 ),
 ( 0.000000000000000000, 1.000000000000000000 ),
 .UNSPECIFIED. ) 
 GEOMETRIC_REPRESENTATION_ITEM ( )  RATIONAL_B_SPLINE_SURFACE ( (
 ( 1.000000000000000000, 0.7071067811865536790, 1.000000000000000000),
 ( 1.000000000000000000, 0.7632447400664059689, 1.000000000000000000),
 ( 1.000000000000000000, 0.8158073005110477727, 1.000000000000000000),
 ( 1.000000000000000000, 0.8906973462395736396, 1.000000000000000000),
 ( 1.000000000000000000, 0.9149408947800440339, 1.000000000000000000),
 ( 1.000000000000000000, 0.9493368785275709820, 1.000000000000000000),
 ( 1.000000000000000000, 0.9605194247156193521, 1.000000000000000000),
 ( 1.000000000000000000, 0.9803630264781763026, 1.000000000000000000),
 ( 1.000000000000000000, 0.9900844824270708111, 1.000000000000000000),
 ( 1.000000000000000000, 0.9894588281429294030, 1.000000000000000000) ) ) 
 REPRESENTATION_ITEM ( '' )  SURFACE ( )  );
#111181=ORIENTED_EDGE ( 'NONE', *, *, #130925, .T. ) ;
#111518=CARTESIAN_POINT ( 'NONE',  ( -18.34374000495059676, 11.47316190337362940, -57.75000000000000711 ) ) ;
#111539=CARTESIAN_POINT ( 'NONE',  ( 12.25000000000000000, 9.850000000011137402, -50.24999999999999289 ) ) ;
#111831=CARTESIAN_POINT ( 'NONE',  ( -16.27683809663751191, 9.350000000011132073, -46.04999999999999716 ) ) ;
#111928=VECTOR ( 'NONE', #18819, 1000.000000000000000 ) ;
#112176=CARTESIAN_POINT ( 'NONE',  ( -16.90202395485831133, 9.965944544561704532, -54.40301372126067037 ) ) ;
#112213=ORIENTED_EDGE ( 'NONE', *, *, #254764, .T. ) ;
#112380=DIRECTION ( 'NONE',  ( -0.000000000000000000, -0.000000000000000000, 1.000000000000000000 ) ) ;
#112540=CARTESIAN_POINT ( 'NONE',  ( 15.66039659514495419, 9.360749169926259938, -50.81457014060725896 ) ) ;
#112729=CARTESIAN_POINT ( 'NONE',  ( 21.72449340488910252, 10.28395627750227703, -46.15000000000001279 ) ) ;
#113120=CARTESIAN_POINT ( 'NONE',  ( -16.94037747912386394, 10.01353938249748587, -46.05113095797549505 ) ) ;
#113158=LINE ( 'NONE', #230549, #185763 ) ;
#113677=DIRECTION ( 'NONE',  ( -0.000000000000000000, -0.000000000000000000, -1.000000000000000000 ) ) ;
#113772=CARTESIAN_POINT ( 'NONE',  ( 20.09999999999999787, 9.750000000011137757, -46.15000000000000568 ) ) ;
#113941=CARTESIAN_POINT ( 'NONE',  ( 15.70340296795548163, 9.355888454513701546, -49.78864289677800770 ) ) ;
#114027=CARTESIAN_POINT ( 'NONE',  ( 20.99999999999999645, 9.750000000011137757, -54.34999999999999432 ) ) ;
#114320=ADVANCED_FACE ( 'NONE', ( #26940 ), #167734, .T. ) ;
#114362=CARTESIAN_POINT ( 'NONE',  ( -16.89155683852518663, 9.950000000011138823, -46.77737184953971905 ) ) ;
#114381=AXIS2_PLACEMENT_3D ( 'NONE', #63200, #219714, #20253 ) ;
#114441=CARTESIAN_POINT ( 'NONE',  ( -16.94107738177415712, 10.01423928514777550, -46.04999999999999716 ) ) ;
#114679=CARTESIAN_POINT ( 'NONE',  ( 18.39999999999999503, 5.650000000011139001, -54.35000000000000142 ) ) ;
#114870=VERTEX_POINT ( 'NONE', #46884 ) ;
#114895=CARTESIAN_POINT ( 'NONE',  ( -16.89268316805465986, 9.951721813253337601, -54.35575247854554704 ) ) ;
#114985=LINE ( 'NONE', #135816, #248714 ) ;
#115061=CARTESIAN_POINT ( 'NONE',  ( -12.26136940704872025, 9.351403174152810749, -50.47953043683849472 ) ) ;
#115304=CARTESIAN_POINT ( 'NONE',  ( -16.95709691156204002, 9.950000000011062440, -54.33994243748958297 ) ) ;
#115325=LINE ( 'NONE', #191047, #199432 ) ;
#115676=DIRECTION ( 'NONE',  ( 1.000000000000000000, 0.000000000000000000, 0.000000000000000000 ) ) ;
#115713=AXIS2_PLACEMENT_3D ( 'NONE', #191435, #12787, #74050 ) ;
#116391=CARTESIAN_POINT ( 'NONE',  ( 12.25000000000000000, 9.350000000011140955, -50.24999999999999289 ) ) ;
#116534=AXIS2_PLACEMENT_3D ( 'NONE', #231930, #252740, #153717 ) ;
#116566=ORIENTED_EDGE ( 'NONE', *, *, #145496, .F. ) ;
#116847=CARTESIAN_POINT ( 'NONE',  ( 20.99999999999999645, 9.750000000011137757, -54.34999999999999432 ) ) ;
#116874=ORIENTED_EDGE ( 'NONE', *, *, #79970, .T. ) ;
#116904=EDGE_LOOP ( 'NONE', ( #181828, #161439, #233638, #74588 ) ) ;
#116927=CARTESIAN_POINT ( 'NONE',  ( -16.96982749440684657, 9.950000000011137047, -46.62477840881235380 ) ) ;
#117237=CARTESIAN_POINT ( 'NONE',  ( -18.40000000000000213, 11.47316190337362762, -46.15000000000000568 ) ) ;
#117401=CARTESIAN_POINT ( 'NONE',  ( 18.54999999999999716, 8.750000000011173285, -46.15000000000000568 ) ) ;
#117431=CARTESIAN_POINT ( 'NONE',  ( 18.54999999999999716, 8.750000000011182166, -54.35000000000000142 ) ) ;
#117470=CARTESIAN_POINT ( 'NONE',  ( -16.94333152882355975, 9.990342011468824168, -54.39203153110149458 ) ) ;
#117626=CARTESIAN_POINT ( 'NONE',  ( -15.66061380678752180, 9.360723793997191677, -50.81392719460674101 ) ) ;
#118019=EDGE_CURVE ( 'NONE', #149704, #98813, #193352, .T. ) ;
#118208=EDGE_CURVE ( 'NONE', #169303, #155471, #235882, .T. ) ;
#118210=CARTESIAN_POINT ( 'NONE',  ( -16.84793658983426212, 9.950000000011137047, -46.23364667781012116 ) ) ;
#118230=AXIS2_PLACEMENT_3D ( 'NONE', #196527, #158726, #175714 ) ;
#118278=AXIS2_PLACEMENT_3D ( 'NONE', #87302, #166893, #28680 ) ;
#118297=CARTESIAN_POINT ( 'NONE',  ( -16.89318236219977010, 9.951535257886288122, -46.14487036789414276 ) ) ;
#118489=DIRECTION ( 'NONE',  ( 1.000000000000000000, 1.186688945009009831E-16, 0.000000000000000000 ) ) ;
#118607=CARTESIAN_POINT ( 'NONE',  ( -17.29838795458461220, 10.37154985795824302, -55.60474128261655125 ) ) ;
#118879=VECTOR ( 'NONE', #70162, 1000.000000000000000 ) ;
#118926=CARTESIAN_POINT ( 'NONE',  ( -15.15564720441980207, 9.410708747058237122, -51.56920840584412957 ) ) ;
#119035=ADVANCED_FACE ( 'NONE', ( #135839 ), #99280, .F. ) ;
#119072=VERTEX_POINT ( 'NONE', #21081 ) ;
#119187=LINE ( 'NONE', #83856, #133460 ) ;
#119417=CARTESIAN_POINT ( 'NONE',  ( -16.97683809663752186, 9.950000000011138823, -53.59763598180368405 ) ) ;
#119432=CARTESIAN_POINT ( 'NONE',  ( -20.65000000000000568, 7.250000000011138646, -42.75000000000000000 ) ) ;
#119576=EDGE_CURVE ( 'NONE', #129130, #219834, #67065, .T. ) ;
#119773=AXIS2_PLACEMENT_3D ( 'NONE', #174342, #152189, #110458 ) ;
#119815=CARTESIAN_POINT ( 'NONE',  ( 15.74999999999999645, 9.350000000011139178, -50.25000000000000000 ) ) ;
#119970=DIRECTION ( 'NONE',  ( -1.000000000000000000, 3.854941057726231589E-15, 0.000000000000000000 ) ) ;
#120029=VERTEX_POINT ( 'NONE', #150653 ) ;
#120080=AXIS2_PLACEMENT_3D ( 'NONE', #174935, #155350, #135737 ) ;
#120082=CARTESIAN_POINT ( 'NONE',  ( -16.87683809663752399, 9.850000000011144508, -53.59763598180369826 ) ) ;
#120473=CYLINDRICAL_SURFACE ( 'NONE', #194902, 14.30833333333333890 ) ;
#120616=CARTESIAN_POINT ( 'NONE',  ( -16.89268316805465986, 9.951721813253337601, -54.35575247854554704 ) ) ;
#120754=CARTESIAN_POINT ( 'NONE',  ( -16.85939591225058720, 9.905226478399001167, -46.46006824646904931 ) ) ;
#120846=CARTESIAN_POINT ( 'NONE',  ( -16.89268316805466341, 9.951721813253341153, -46.14424752145445296 ) ) ;
#121090=ORIENTED_EDGE ( 'NONE', *, *, #157249, .T. ) ;
#121399=ORIENTED_EDGE ( 'NONE', *, *, #197841, .F. ) ;
#121683=DIRECTION ( 'NONE',  ( -3.035766082959430717E-14, 0.000000000000000000, -1.000000000000000000 ) ) ;
#121818=EDGE_CURVE ( 'NONE', #136044, #216000, #106159, .T. ) ;
#121952=CARTESIAN_POINT ( 'NONE',  ( -12.60206096961792532, 9.389686005666810331, -49.17284350635132029 ) ) ;
#121975=ORIENTED_EDGE ( 'NONE', *, *, #168028, .T. ) ;
#122283=CARTESIAN_POINT ( 'NONE',  ( -16.94445028196807002, 9.992063609708893068, -54.39266982158155628 ) ) ;
#122428=CARTESIAN_POINT ( 'NONE',  ( -20.65000000000000568, 5.650000000011139001, -42.75000000000000000 ) ) ;
#122467=MECHANICAL_DESIGN_GEOMETRIC_PRESENTATION_REPRESENTATION('',(#22518),#196898);
#122683=ORIENTED_EDGE ( 'NONE', *, *, #241128, .F. ) ;
#123111=PLANE ( 'NONE',  #45335 ) ;
#123176=VERTEX_POINT ( 'NONE', #36984 ) ;
#123217=B_SPLINE_CURVE_WITH_KNOTS ( 'NONE', 3,
 ( #236338, #57686, #232515, #135937 ),
 .UNSPECIFIED., .F., .F.,
 ( 4, 4 ),
 ( 0.000000000000000000, 7.713889350927600000E-05 ),
 .UNSPECIFIED. ) ;
#123233=CARTESIAN_POINT ( 'NONE',  ( -12.47155713865592652, 9.375669526436931633, -49.36779000938595630 ) ) ;
#123899=VERTEX_POINT ( 'NONE', #74225 ) ;
#123928=VECTOR ( 'NONE', #60010, 1000.000000000000000 ) ;
#123938=ADVANCED_FACE ( 'NONE', ( #33823 ), #95085, .T. ) ;
#124104=EDGE_LOOP ( 'NONE', ( #217851, #238753, #180094, #99148, #63321 ) ) ;
#124111=ORIENTED_EDGE ( 'NONE', *, *, #104147, .F. ) ;
#124202=PRODUCT_DEFINITION_SHAPE ( 'NONE', 'NONE',  #182404 ) ;
#124415=ORIENTED_EDGE ( 'NONE', *, *, #44939, .F. ) ;
#124461=FACE_OUTER_BOUND ( 'NONE', #2531, .T. ) ;
#124462=B_SPLINE_CURVE_WITH_KNOTS ( 'NONE', 3,
 ( #172739, #95706, #215650, #34491, #91865, #211828, #94424, #76146, #55273, #235230 ),
 .UNSPECIFIED., .F., .F.,
 ( 4, 3, 3, 4 ),
 ( 1.957469226477651626E-15, 8.145022132832446376E-06, 1.905645951092409121E-05, 2.061107371225752961E-05 ),
 .UNSPECIFIED. ) ;
#124515=ORIENTED_EDGE ( 'NONE', *, *, #96077, .T. ) ;
#124684=CARTESIAN_POINT ( 'NONE',  ( -18.40000000000000213, 5.650000000011139001, -57.75000000000000711 ) ) ;
#125168=ORIENTED_EDGE ( 'NONE', *, *, #127715, .T. ) ;
#125309=DIRECTION ( 'NONE',  ( 1.000000000000000000, 0.000000000000000000, 1.073024830501117725E-15 ) ) ;
#125401=EDGE_CURVE ( 'NONE', #21668, #936, #225721, .T. ) ;
#125837=DIRECTION ( 'NONE',  ( 1.000000000000000000, -0.000000000000000000, -0.000000000000000000 ) ) ;
#125847=CARTESIAN_POINT ( 'NONE',  ( 18.39999999999999503, 11.75000000001113953, -54.35000000000000142 ) ) ;
#125857=ORIENTED_EDGE ( 'NONE', *, *, #172080, .T. ) ;
#125942=CARTESIAN_POINT ( 'NONE',  ( -23.25000000000000355, 5.650000000011139001, -42.75000000000000000 ) ) ;
#126098=PLANE ( 'NONE',  #153439 ) ;
#126099=CARTESIAN_POINT ( 'NONE',  ( 15.48841904831874849, 8.561580951692381092, -46.14999999999999858 ) ) ;
#126420=FACE_OUTER_BOUND ( 'NONE', #20418, .T. ) ;
#126514=CARTESIAN_POINT ( 'NONE',  ( -16.97683809663752186, 9.950000000011138823, -53.59763598180368405 ) ) ;
#126571=VERTEX_POINT ( 'NONE', #1281 ) ;
#126587=CARTESIAN_POINT ( 'NONE',  ( 18.39999999999999503, 5.650000000011139001, -54.35000000000000142 ) ) ;
#126718=EDGE_CURVE ( 'NONE', #180781, #114870, #39171, .T. ) ;
#126802=CARTESIAN_POINT ( 'NONE',  ( 18.54999999999999716, 8.750000000011182166, -54.35000000000000142 ) ) ;
#126877=DIRECTION ( 'NONE',  ( 1.000000000000000000, 0.000000000000000000, -0.000000000000000000 ) ) ;
#126945=DIRECTION ( 'NONE',  ( -1.000000000000000000, 0.000000000000000000, 0.000000000000000000 ) ) ;
#126962=CARTESIAN_POINT ( 'NONE',  ( -16.87683809663752399, 9.850000000011140955, -46.15000000000000568 ) ) ;
#127309=CARTESIAN_POINT ( 'NONE',  ( -16.79184697841823493, 9.948761661669548673, -46.15414227060252728 ) ) ;
#127316=CARTESIAN_POINT ( 'NONE',  ( 18.54999999999999716, 8.750000000011182166, -46.15000000000000568 ) ) ;
#127380=VERTEX_POINT ( 'NONE', #43352 ) ;
#127407=FACE_OUTER_BOUND ( 'NONE', #179335, .T. ) ;
#127412=VECTOR ( 'NONE', #32213, 1000.000000000000000 ) ;
#127715=EDGE_CURVE ( 'NONE', #67166, #119072, #217793, .T. ) ;
#127871=CARTESIAN_POINT ( 'NONE',  ( -16.89146115310546037, 9.951443245667611848, -54.35482241895421396 ) ) ;
#127947=LINE ( 'NONE', #187926, #228276 ) ;
#127963=CARTESIAN_POINT ( 'NONE',  ( -16.80939487329394666, 9.950000000011138823, -54.35000000000088249 ) ) ;
#128038=ORIENTED_EDGE ( 'NONE', *, *, #82601, .T. ) ;
#128164=CARTESIAN_POINT ( 'NONE',  ( 23.04999999999999716, 8.822561741677553471, -57.75000000000000000 ) ) ;
#128181=CARTESIAN_POINT ( 'NONE',  ( -16.85697194749128514, 9.908543714134763647, -54.06499573238597378 ) ) ;
#128354=VERTEX_POINT ( 'NONE', #98351 ) ;
#128462=CARTESIAN_POINT ( 'NONE',  ( -16.86578989773641979, 9.984809801269951990, -46.03533511337776929 ) ) ;
#128515=CARTESIAN_POINT ( 'NONE',  ( -18.35668295345803713, 11.47316190337363118, -57.75000000000000711 ) ) ;
#128869=DIRECTION ( 'NONE',  ( 0.2834754621636358940, -0.2834754621636437211, 0.9161240771326893961 ) ) ;
#128908=CARTESIAN_POINT ( 'NONE',  ( -18.40000000000000213, 5.650000000011139001, -46.15000000000000568 ) ) ;
#129064=EDGE_LOOP ( 'NONE', ( #32165, #68068 ) ) ;
#129085=CARTESIAN_POINT ( 'NONE',  ( -16.86133551771148475, 9.950000000011137047, -54.30134343454665924 ) ) ;
#129130=VERTEX_POINT ( 'NONE', #231064 ) ;
#129226=B_SPLINE_CURVE_WITH_KNOTS ( 'NONE', 3,
 ( #120082, #236142, #176192, #254390, #174945, #60061, #198295, #195761, #75789, #139582, #138299, #37967, #199611, #240005 ),
 .UNSPECIFIED., .F., .F.,
 ( 4, 2, 2, 2, 2, 2, 4 ),
 ( 1.398578778534940505E-17, 0.0003823333598417805049, 0.0005735000397626734137, 0.0006690833797231096223, 0.0007168750497033291903, 0.0007407708846934367517, 0.0007646667196835443131 ),
 .UNSPECIFIED. ) ;
#129466=CARTESIAN_POINT ( 'NONE',  ( -16.96982749440705973, 9.950000000011137047, -53.87522159118827858 ) ) ;
#129531=LINE ( 'NONE', #86509, #217834 ) ;
#129623=CARTESIAN_POINT ( 'NONE',  ( 21.13736287352038445, 8.046642376395153562, -42.75000000000000000 ) ) ;
#129691=VERTEX_POINT ( 'NONE', #240670 ) ;
#129790=DIRECTION ( 'NONE',  ( 1.000000000000000000, 1.186688945009010077E-16, 0.000000000000000000 ) ) ;
#129857=ORIENTED_EDGE ( 'NONE', *, *, #169743, .F. ) ;
#129914=VERTEX_POINT ( 'NONE', #77419 ) ;
#129945=LINE ( 'NONE', #12613, #132548 ) ;
#130011=CARTESIAN_POINT ( 'NONE',  ( -18.39999999999999858, 11.75000000001113953, -42.75000000000000000 ) ) ;
#130098=CARTESIAN_POINT ( 'NONE',  ( 17.23472005113827876, 10.30788195451192024, -44.95342313993132422 ) ) ;
#130284=ORIENTED_EDGE ( 'NONE', *, *, #240143, .T. ) ;
#130375=ADVANCED_FACE ( 'NONE', ( #161844 ), #64612, .T. ) ;
#130392=AXIS2_PLACEMENT_3D ( 'NONE', #6920, #164722, #89020 ) ;
#130520=EDGE_CURVE ( 'NONE', #165658, #73622, #66180, .T. ) ;
#130623=EDGE_LOOP ( 'NONE', ( #224587, #29788, #231490, #54433, #184915, #239970, #251311, #61136, #92635, #169406, #39403, #145390, #229448, #250801, #19, #28730, #66594, #162612 ) ) ;
#130925=EDGE_CURVE ( 'NONE', #239517, #219834, #111091, .T. ) ;
#131143=VECTOR ( 'NONE', #248121, 1000.000000000000000 ) ;
#131279=ORIENTED_EDGE ( 'NONE', *, *, #213195, .F. ) ;
#131287=LINE ( 'NONE', #13921, #127412 ) ;
#131288=VERTEX_POINT ( 'NONE', #109873 ) ;
#131650=FACE_OUTER_BOUND ( 'NONE', #52574, .T. ) ;
#131724=ADVANCED_FACE ( 'NONE', ( #167032 ), #30083, .F. ) ;
#132071=SURFACE_STYLE_USAGE ( .BOTH. , #52516 ) ;
#132154=CARTESIAN_POINT ( 'NONE',  ( -16.87331047859649757, 9.950000000011138823, -54.35000000000000142 ) ) ;
#132224=CARTESIAN_POINT ( 'NONE',  ( -18.40000000000000213, 11.47316190337364183, -57.67405393319205587 ) ) ;
#132253=AXIS2_PLACEMENT_3D ( 'NONE', #245376, #27640, #146249 ) ;
#132548=VECTOR ( 'NONE', #232945, 1000.000000000000000 ) ;
#132827=CARTESIAN_POINT ( 'NONE',  ( 23.24999999999999645, 11.75000000001113953, -54.34999999999999432 ) ) ;
#132925=VERTEX_POINT ( 'NONE', #117431 ) ;
#133381=PLANE ( 'NONE',  #225723 ) ;
#133398=LINE ( 'NONE', #192100, #184162 ) ;
#133413=DIRECTION ( 'NONE',  ( -1.000000000000000000, 0.000000000000000000, 0.000000000000000000 ) ) ;
#133460=VECTOR ( 'NONE', #40957, 1000.000000000000000 ) ;
#133952=CARTESIAN_POINT ( 'NONE',  ( -16.93440969289731157, 9.995185175825110235, -46.09123418501079783 ) ) ;
#134208=CARTESIAN_POINT ( 'NONE',  ( -18.39999999999999858, 11.47316190337362762, -42.82594606680797256 ) ) ;
#134264=DIRECTION ( 'NONE',  ( 1.000000000000000000, 0.000000000000000000, 0.000000000000000000 ) ) ;
#134352=CARTESIAN_POINT ( 'NONE',  ( 23.24999999999999645, 8.822561741677553471, -42.75000000000000000 ) ) ;
#134516=VECTOR ( 'NONE', #81101, 1000.000000000000000 ) ;
#135084=B_SPLINE_CURVE_WITH_KNOTS ( 'NONE', 3,
 ( #165660, #245183, #129085, #225582, #46951, #27457, #169536, #9137, #168252, #126514 ),
 .UNSPECIFIED., .F., .F.,
 ( 4, 2, 2, 2, 4 ),
 ( 5.259846352425386116E-16, 9.930191194500028547E-05, 0.0001986038238894745702, 0.0003972076477784231940, 0.0007944152955563411498 ),
 .UNSPECIFIED. ) ;
#135100=CARTESIAN_POINT ( 'NONE',  ( 20.99999999999999645, 9.750000000011137757, -46.15000000000000568 ) ) ;
#135160=DIRECTION ( 'NONE',  ( 0.000000000000000000, 0.000000000000000000, 1.000000000000000000 ) ) ;
#135224=ORIENTED_EDGE ( 'NONE', *, *, #88032, .F. ) ;
#135356=DIRECTION ( 'NONE',  ( -1.000000000000000000, -0.000000000000000000, -0.000000000000000000 ) ) ;
#135737=DIRECTION ( 'NONE',  ( -1.000000000000000000, 0.000000000000000000, 0.000000000000000000 ) ) ;
#135816=CARTESIAN_POINT ( 'NONE',  ( 18.39999999999999503, 11.47316190337363828, -46.15000000000000568 ) ) ;
#135839=FACE_OUTER_BOUND ( 'NONE', #239118, .T. ) ;
#135937=CARTESIAN_POINT ( 'NONE',  ( -18.40000000000000213, 11.47316190337364183, -57.67405393319205587 ) ) ;
#136044=VERTEX_POINT ( 'NONE', #224828 ) ;
#136141=DIRECTION ( 'NONE',  ( -1.020425574104004196E-15, 0.000000000000000000, 1.000000000000000000 ) ) ;
#136839=CLOSED_SHELL ( 'NONE', ( #53945, #90226, #155636, #91001, #98896, #72341, #46396, #254262, #31002, #187655, #174951, #29863, #16471, #250424, #78235, #149163, #85740, #140295, #186484, #213405, #67155, #71970, #246545, #104936, #70461, #109432, #131724, #91741, #168694, #119035, #154394, #158653, #150601, #89461, #186353, #228284, #240482, #190804, #200349, #68602, #74133, #224330, #159942, #165791, #235402, #130375, #194749, #114320, #123938, #174020, #158114, #180073, #1115 ) ) ;
#136862=CARTESIAN_POINT ( 'NONE',  ( -17.73285935861159501, 10.85798180380402300, -56.75856180978417598 ) ) ;
#136935=B_SPLINE_CURVE_WITH_KNOTS ( 'NONE', 3,
 ( #134208, #13021, #177231, #57226 ),
 .UNSPECIFIED., .F., .F.,
 ( 4, 4 ),
 ( 0.000000000000000000, 7.713889350929433657E-05 ),
 .UNSPECIFIED. ) ;
#136966=DIRECTION ( 'NONE',  ( 0.000000000000000000, -1.000000000000000000, 0.000000000000000000 ) ) ;
#137027=VERTEX_POINT ( 'NONE', #2908 ) ;
#137250=ORIENTED_EDGE ( 'NONE', *, *, #229472, .F. ) ;
#137251=CARTESIAN_POINT ( 'NONE',  ( -18.40000000000000213, 11.75000000001113953, -46.15000000000000568 ) ) ;
#137289=APPLICATION_CONTEXT ( 'automotive_design' ) ;
#137301=EDGE_CURVE ( 'NONE', #128354, #168945, #161716, .T. ) ;
#137436=DIRECTION ( 'NONE',  ( 1.000000000000000000, 0.000000000000000000, 0.000000000000000000 ) ) ;
#137647=ORIENTED_EDGE ( 'NONE', *, *, #165022, .T. ) ;
#137750=CARTESIAN_POINT ( 'NONE',  ( -16.88705144915432044, 9.950000000011137047, -46.43097859471209432 ) ) ;
#137911=CARTESIAN_POINT ( 'NONE',  ( 18.39999999999999503, 11.75000000001113953, -57.75000000000000711 ) ) ;
#137998=CARTESIAN_POINT ( 'NONE',  ( -23.25000000000000355, 11.75000000001113953, -42.75000000000000000 ) ) ;
#138052=DIRECTION ( 'NONE',  ( 1.186688945009009831E-16, -1.000000000000000000, 0.000000000000000000 ) ) ;
#138089=VECTOR ( 'NONE', #12528, 1000.000000000000000 ) ;
#138197=DIRECTION ( 'NONE',  ( -0.000000000000000000, -0.000000000000000000, -1.000000000000000000 ) ) ;
#138281=CARTESIAN_POINT ( 'NONE',  ( -16.94275863006528482, 9.989496048678669027, -54.39169738207657900 ) ) ;
#138299=CARTESIAN_POINT ( 'NONE',  ( -16.80100914604134132, 9.943149094114719588, -54.31704412728765874 ) ) ;
#138374=CARTESIAN_POINT ( 'NONE',  ( -17.80356949363890706, 10.87673139701253788, -43.78692697577277215 ) ) ;
#138644=CARTESIAN_POINT ( 'NONE',  ( -18.35663730107557257, 11.47390742652235573, -42.75000000000000000 ) ) ;
#139140=FACE_OUTER_BOUND ( 'NONE', #167283, .T. ) ;
#139398=CARTESIAN_POINT ( 'NONE',  ( -16.94275863009466576, 9.989496048673542461, -46.10830261795888418 ) ) ;
#139509=CARTESIAN_POINT ( 'NONE',  ( 21.72449340488909897, 10.28395627750227703, -54.34999999999999432 ) ) ;
#139582=CARTESIAN_POINT ( 'NONE',  ( -16.80469485234340965, 9.942151663152193564, -54.30996684393117846 ) ) ;
#139734=CARTESIAN_POINT ( 'NONE',  ( -15.39126916658602973, 9.389571634557563939, -51.31764071236917601 ) ) ;
#139775=CARTESIAN_POINT ( 'NONE',  ( 16.27683809663750125, 9.350000000011137402, -42.75000000000000000 ) ) ;
#139867=CARTESIAN_POINT ( 'NONE',  ( -17.11825945287481332, 10.05000000001113847, -54.35000000000000142 ) ) ;
#139868=CARTESIAN_POINT ( 'NONE',  ( -15.75000000000000355, 9.350000000011140955, -50.25000000000000711 ) ) ;
#140011=DIRECTION ( 'NONE',  ( -0.000000000000000000, 1.000000000000000000, -0.000000000000000000 ) ) ;
#140167=FACE_OUTER_BOUND ( 'NONE', #6375, .T. ) ;
#140295=ADVANCED_FACE ( 'NONE', ( #126420 ), #105538, .F. ) ;
#140402=CARTESIAN_POINT ( 'NONE',  ( -16.85718274719427257, 9.976142314632859609, -46.06334633218259000 ) ) ;
#140734=CIRCLE ( 'NONE', #28346, 1.749999999999998002 ) ;
#140741=CARTESIAN_POINT ( 'NONE',  ( 20.99999999999999645, 9.750000000011137757, -42.75000000000000000 ) ) ;
#140828=CARTESIAN_POINT ( 'NONE',  ( -18.40000000000000213, 11.75000000001113953, -57.75000000000000000 ) ) ;
#140849=CARTESIAN_POINT ( 'NONE',  ( -21.65000000000000213, 7.250000000011138646, -42.75000000000000000 ) ) ;
#141210=VERTEX_POINT ( 'NONE', #172368 ) ;
#141263=EDGE_CURVE ( 'NONE', #123899, #97258, #129226, .T. ) ;
#141421=ORIENTED_EDGE ( 'NONE', *, *, #34063, .F. ) ;
#141471=EDGE_CURVE ( 'NONE', #22095, #144454, #53348, .T. ) ;
#141521=( BOUNDED_SURFACE ( )  B_SPLINE_SURFACE ( 3, 2, ( 
 ( #230841, #229544, #190431 ),
 ( #71763, #191723, #189124 ),
 ( #32664, #112176, #212554 ),
 ( #10496, #53465, #13076 ) ),
 .UNSPECIFIED., .F., .F., .F. ) 
 B_SPLINE_SURFACE_WITH_KNOTS ( ( 4, 4 ),
 ( 3, 3 ),
 ( 0.0008258556059633754111, 0.0009616864997632785118 ),
 ( 0.000000000000000000, 1.000000000000000000 ),
 .UNSPECIFIED. ) 
 GEOMETRIC_REPRESENTATION_ITEM ( )  RATIONAL_B_SPLINE_SURFACE ( (
 ( 1.000000000000000000, 0.9152888060719349683, 1.000000000000000000),
 ( 1.000000000000000000, 0.9327727094138323904, 1.000000000000000000),
 ( 1.000000000000000000, 0.9369023509258284088, 1.000000000000000000),
 ( 1.000000000000000000, 0.9246339933864518024, 1.000000000000000000) ) ) 
 REPRESENTATION_ITEM ( '' )  SURFACE ( )  );
#141542=ORIENTED_EDGE ( 'NONE', *, *, #149989, .F. ) ;
#141831=CARTESIAN_POINT ( 'NONE',  ( -16.93344882324368683, 9.996588767299030565, -54.41302569480492224 ) ) ;
#141877=PLANE ( 'NONE',  #81675 ) ;
#141912=EDGE_CURVE ( 'NONE', #137027, #9728, #131287, .T. ) ;
#142207=ORIENTED_EDGE ( 'NONE', *, *, #149482, .T. ) ;
#142769=CARTESIAN_POINT ( 'NONE',  ( -13.54795643572458452, 9.450668889178684751, -48.55554649020736235 ) ) ;
#142778=DIRECTION ( 'NONE',  ( -0.5932847527679298016, 0.8049926720990051576, 0.000000000000000000 ) ) ;
#142825=CARTESIAN_POINT ( 'NONE',  ( -16.78493832629887450, 9.945835743215301505, -46.16394901910420856 ) ) ;
#142960=CARTESIAN_POINT ( 'NONE',  ( 15.31784899511109543, 9.396630376328870327, -51.40705739281828812 ) ) ;
#143007=LINE ( 'NONE', #67348, #162013 ) ;
#143105=CARTESIAN_POINT ( 'NONE',  ( -16.94132844910802405, 9.992436755191501874, -54.39620175598232521 ) ) ;
#143276=DIRECTION ( 'NONE',  ( 0.000000000000000000, -0.9553114395362780620, -0.2956011730205483912 ) ) ;
#143296=COLOUR_RGB ( '', 0.40784314, 0.44705882, 0.49803922) ;
#143558=DIRECTION ( 'NONE',  ( -1.020425574104004196E-15, 0.000000000000000000, -1.000000000000000000 ) ) ;
#143756=VERTEX_POINT ( 'NONE', #211158 ) ;
#143783=( BOUNDED_SURFACE ( )  B_SPLINE_SURFACE ( 3, 2, ( 
 ( #114441, #247534, #197814 ),
 ( #16636, #175720, #140402 ),
 ( #98676, #239525, #255168 ),
 ( #238225, #38758, #118297 ) ),
 .UNSPECIFIED., .F., .F., .F. ) 
 B_SPLINE_SURFACE_WITH_KNOTS ( ( 4, 4 ),
 ( 3, 3 ),
 ( 0.0008258556059633777964, 0.0009616864997632780781 ),
 ( 0.000000000000000000, 1.000000000000000000 ),
 .UNSPECIFIED. ) 
 GEOMETRIC_REPRESENTATION_ITEM ( )  RATIONAL_B_SPLINE_SURFACE ( (
 ( 1.000000000000000000, 0.9152888060719349683, 1.000000000000000000),
 ( 1.000000000000000000, 0.9327727094138136277, 1.000000000000000000),
 ( 1.000000000000000000, 0.9369023509258470606, 1.000000000000000000),
 ( 1.000000000000000000, 0.9246339933864458072, 1.000000000000000000) ) ) 
 REPRESENTATION_ITEM ( '' )  SURFACE ( )  );
#143801=CARTESIAN_POINT ( 'NONE',  ( -18.38639463286148867, 11.48019957384713230, -42.75000000000000000 ) ) ;
#144041=CARTESIAN_POINT ( 'NONE',  ( -23.25000000000000355, 5.650000000011139001, -46.15000000000000568 ) ) ;
#144128=FACE_OUTER_BOUND ( 'NONE', #54957, .T. ) ;
#144374=CARTESIAN_POINT ( 'NONE',  ( -16.93294127766158752, 10.00328010296601811, -54.42990726582922889 ) ) ;
#144415=CARTESIAN_POINT ( 'NONE',  ( -18.40000000000000213, 11.47316190337362762, -46.04999999999999716 ) ) ;
#144454=VERTEX_POINT ( 'NONE', #112729 ) ;
#144584=ORIENTED_EDGE ( 'NONE', *, *, #26683, .T. ) ;
#144630=AXIS2_PLACEMENT_3D ( 'NONE', #119432, #41192, #101082 ) ;
#144669=ORIENTED_EDGE ( 'NONE', *, *, #224617, .T. ) ;
#144797=VERTEX_POINT ( 'NONE', #232394 ) ;
#144817=ORIENTED_EDGE ( 'NONE', *, *, #245717, .F. ) ;
#144851=CARTESIAN_POINT ( 'NONE',  ( 18.39999999999997371, 11.75000000001113953, -42.75000000000000000 ) ) ;
#144909=DIRECTION ( 'NONE',  ( 1.000000000000000000, -0.000000000000000000, -0.000000000000000000 ) ) ;
#145052=LINE ( 'NONE', #108500, #77667 ) ;
#145063=ORIENTED_EDGE ( 'NONE', *, *, #245442, .T. ) ;
#145077=ORIENTED_EDGE ( 'NONE', *, *, #118208, .T. ) ;
#145151=CARTESIAN_POINT ( 'NONE',  ( -16.87683809663752399, 9.850000000011139178, -53.59763598180368405 ) ) ;
#145220=EDGE_LOOP ( 'NONE', ( #186425, #95587, #13145, #29564 ) ) ;
#145275=CARTESIAN_POINT ( 'NONE',  ( -16.86379686415369150, 9.975217759264314310, -54.43338988909027876 ) ) ;
#145382=VERTEX_POINT ( 'NONE', #209293 ) ;
#145390=ORIENTED_EDGE ( 'NONE', *, *, #19918, .F. ) ;
#145496=EDGE_CURVE ( 'NONE', #239517, #52893, #115325, .T. ) ;
#145499=CARTESIAN_POINT ( 'NONE',  ( -18.34374000495059676, 11.47316190337362940, -57.75000000000000711 ) ) ;
#145516=ORIENTED_EDGE ( 'NONE', *, *, #148122, .F. ) ;
#145527=AXIS2_PLACEMENT_3D ( 'NONE', #195649, #178665, #119970 ) ;
#145688=ORIENTED_EDGE ( 'NONE', *, *, #27033, .T. ) ;
#145813=CARTESIAN_POINT ( 'NONE',  ( -16.94309007106720344, 9.992226192581140864, -46.10579128255550785 ) ) ;
#146249=DIRECTION ( 'NONE',  ( 1.000000000000000000, 0.000000000000000000, 0.000000000000000000 ) ) ;
#146675=CARTESIAN_POINT ( 'NONE',  ( -16.80468759584938354, 9.942153675145293690, -46.19001886620164044 ) ) ;
#147433=DIRECTION ( 'NONE',  ( -1.073024830501117725E-15, 0.000000000000000000, 1.000000000000000000 ) ) ;
#147485=LINE ( 'NONE', #190491, #49361 ) ;
#147519=CARTESIAN_POINT ( 'NONE',  ( -16.81744102076748959, 9.950000000011138823, -54.35000000000000142 ) ) ;
#147665=VECTOR ( 'NONE', #157468, 1000.000000000000000 ) ;
#147729=DIRECTION ( 'NONE',  ( -0.000000000000000000, -0.000000000000000000, -1.000000000000000000 ) ) ;
#147747=CARTESIAN_POINT ( 'NONE',  ( -16.88783316861814754, 9.950000000011137047, -54.24773595802036397 ) ) ;
#147800=PLANE ( 'NONE',  #199098 ) ;
#148028=CARTESIAN_POINT ( 'NONE',  ( -16.86757978335471364, 9.965650379045438712, -46.09800465316752138 ) ) ;
#148122=EDGE_CURVE ( 'NONE', #114870, #47719, #161083, .T. ) ;
#148402=DIRECTION ( 'NONE',  ( 0.000000000000000000, 0.000000000000000000, -1.000000000000000000 ) ) ;
#148421=VECTOR ( 'NONE', #201522, 999.9999999999998863 ) ;
#148960=FACE_OUTER_BOUND ( 'NONE', #255203, .T. ) ;
#149163=ADVANCED_FACE ( 'NONE', ( #2018 ), #82820, .F. ) ;
#149409=EDGE_CURVE ( 'NONE', #137027, #145382, #232338, .T. ) ;
#149482=EDGE_CURVE ( 'NONE', #154908, #143756, #54271, .T. ) ;
#149487=VECTOR ( 'NONE', #50630, 1000.000000000000000 ) ;
#149703=ORIENTED_EDGE ( 'NONE', *, *, #26683, .F. ) ;
#149704=VERTEX_POINT ( 'NONE', #32899 ) ;
#149705=CARTESIAN_POINT ( 'NONE',  ( -17.11825945287482753, 10.05000000001113847, -46.25000000000000711 ) ) ;
#149778=DIRECTION ( 'NONE',  ( 0.000000000000000000, 0.000000000000000000, -1.000000000000000000 ) ) ;
#149833=CARTESIAN_POINT ( 'NONE',  ( -16.81744102076748959, 9.950000000011138823, -54.35000000000000142 ) ) ;
#149877=VERTEX_POINT ( 'NONE', #60102 ) ;
#149946=B_SPLINE_CURVE_WITH_KNOTS ( 'NONE', 3,
 ( #246889, #231213, #250745, #52540, #112540, #192085, #82977, #63440, #142960, #222499, #43892, #107379, #186957, #8309, #167392, #94240, #14742, #155543, #17294, #254574, #253312, #95527, #13438, #232500, #74729, #154274, #214203, #75972, #35590, #116391 ),
 .UNSPECIFIED., .F., .F.,
 ( 4, 2, 2, 2, 2, 2, 2, 2, 2, 2, 2, 2, 2, 2, 4 ),
 ( 0.000000000000000000, 0.0003422764154113336690, 0.0006845528308226673381, 0.001026829246234001007, 0.001369105661645334676, 0.002053658492468005917, 0.002738211323290676725, 0.003080487738702009960, 0.003422764154113342762, 0.003765040569524675997, 0.004107316984936009233, 0.004449593400347342034, 0.004791869815758674836, 0.005134146231170008505, 0.005476422646581341307 ),
 .UNSPECIFIED. ) ;
#149989=EDGE_CURVE ( 'NONE', #215894, #71372, #135084, .T. ) ;
#150000=ORIENTED_EDGE ( 'NONE', *, *, #3728, .F. ) ;
#150022=CARTESIAN_POINT ( 'NONE',  ( -14.00000000000000178, 9.850000000011133849, -50.25000000000000711 ) ) ;
#150372=FACE_OUTER_BOUND ( 'NONE', #155683, .T. ) ;
#150392=DIRECTION ( 'NONE',  ( -1.000000000000000000, 0.000000000000000000, 0.000000000000000000 ) ) ;
#150471=ORIENTED_EDGE ( 'NONE', *, *, #38836, .F. ) ;
#150519=CARTESIAN_POINT ( 'NONE',  ( 13.54556439290363912, 9.450592112144857282, -48.55618831880837405 ) ) ;
#150601=ADVANCED_FACE ( 'NONE', ( #4324, #162154, #164705 ), #120473, .T. ) ;
#150648=VERTEX_POINT ( 'NONE', #103414 ) ;
#150653=CARTESIAN_POINT ( 'NONE',  ( 18.54999999999999716, 9.950000000011153034, -54.35000000000005826 ) ) ;
#150718=B_SPLINE_CURVE_WITH_KNOTS ( 'NONE', 3,
 ( #245253, #10494, #186570, #48321, #26210, #230840, #168323, #127871, #66611, #170898 ),
 .UNSPECIFIED., .F., .F.,
 ( 4, 3, 3, 4 ),
 ( 0.000000000000000000, 1.004626015991478527E-05, 1.831183478183247374E-05, 2.062343583996109511E-05 ),
 .UNSPECIFIED. ) ;
#150960=CARTESIAN_POINT ( 'NONE',  ( 18.39999999999998082, 11.47316190337362585, -42.75000000000000000 ) ) ;
#151054=CARTESIAN_POINT ( 'NONE',  ( 20.09999999999999787, 9.750000000011137757, -42.75000000000000000 ) ) ;
#151625=CARTESIAN_POINT ( 'NONE',  ( -16.77308656112214535, 9.950000000011137047, -54.34980680829769994 ) ) ;
#151638=VERTEX_POINT ( 'NONE', #61889 ) ;
#151853=DIRECTION ( 'NONE',  ( 1.186688945009009831E-16, -1.000000000000000000, 0.000000000000000000 ) ) ;
#151928=ORIENTED_EDGE ( 'NONE', *, *, #126718, .F. ) ;
#151965=VERTEX_POINT ( 'NONE', #81125 ) ;
#152161=AXIS2_PLACEMENT_3D ( 'NONE', #161327, #24388, #240854 ) ;
#152189=DIRECTION ( 'NONE',  ( 0.000000000000000000, 0.000000000000000000, 1.000000000000000000 ) ) ;
#152207=ORIENTED_EDGE ( 'NONE', *, *, #195767, .T. ) ;
#152558=ORIENTED_EDGE ( 'NONE', *, *, #253155, .F. ) ;
#152570=CIRCLE ( 'NONE', #177511, 0.1999999999999987899 ) ;
#152757=VERTEX_POINT ( 'NONE', #137911 ) ;
#152769=CARTESIAN_POINT ( 'NONE',  ( -16.90987985657661952, 9.957807518190886498, -54.36928708888363815 ) ) ;
#152846=FACE_OUTER_BOUND ( 'NONE', #167864, .T. ) ;
#152956=( LENGTH_UNIT ( ) NAMED_UNIT ( * ) SI_UNIT ( .MILLI., .METRE. ) );
#153405=VECTOR ( 'NONE', #62934, 1000.000000000000000 ) ;
#153420=ORIENTED_EDGE ( 'NONE', *, *, #184211, .T. ) ;
#153429=LINE ( 'NONE', #231653, #155453 ) ;
#153439=AXIS2_PLACEMENT_3D ( 'NONE', #4850, #243490, #205635 ) ;
#153513=CARTESIAN_POINT ( 'NONE',  ( 0.000000000000000000, 0.000000000000000000, 0.000000000000000000 ) ) ;
#153581=CARTESIAN_POINT ( 'NONE',  ( -16.93772744219066340, 9.993541108763512426, -46.09806197196969890 ) ) ;
#153717=DIRECTION ( 'NONE',  ( -1.186688945009010077E-16, 1.000000000000000000, 0.000000000000000000 ) ) ;
#153905=CARTESIAN_POINT ( 'NONE',  ( 18.54999999999999716, 8.750000000011182166, -42.75000000000000000 ) ) ;
#154165=CARTESIAN_POINT ( 'NONE',  ( -21.64999999999999858, 10.05000000001113847, -46.25000000000000711 ) ) ;
#154235=CARTESIAN_POINT ( 'NONE',  ( -12.30589683808040391, 9.356746017089404788, -50.70335972136417979 ) ) ;
#154274=CARTESIAN_POINT ( 'NONE',  ( 12.33938619321247820, 9.360723793997193454, -50.81392719460670548 ) ) ;
#154394=ADVANCED_FACE ( 'NONE', ( #73430 ), #133381, .F. ) ;
#154406=ORIENTED_EDGE ( 'NONE', *, *, #221160, .F. ) ;
#154715=ORIENTED_EDGE ( 'NONE', *, *, #68118, .F. ) ;
#154729=LINE ( 'NONE', #32210, #52084 ) ;
#154891=VECTOR ( 'NONE', #18184, 1000.000000000000000 ) ;
#154908=VERTEX_POINT ( 'NONE', #210327 ) ;
#155036=CARTESIAN_POINT ( 'NONE',  ( -17.04295772865462766, 10.02489942527107303, -46.14999999999999858 ) ) ;
#155061=ORIENTED_EDGE ( 'NONE', *, *, #5973, .T. ) ;
#155114=VERTEX_POINT ( 'NONE', #113772 ) ;
#155319=AXIS2_PLACEMENT_3D ( 'NONE', #156257, #218742, #255266 ) ;
#155350=DIRECTION ( 'NONE',  ( -0.000000000000000000, -0.000000000000000000, -1.000000000000000000 ) ) ;
#155453=VECTOR ( 'NONE', #13876, 1000.000000000000000 ) ;
#155471=VERTEX_POINT ( 'NONE', #230880 ) ;
#155506=CARTESIAN_POINT ( 'NONE',  ( -13.54036565897074951, 9.451541661396669625, -51.95387549883059819 ) ) ;
#155543=CARTESIAN_POINT ( 'NONE',  ( 13.22461703343584816, 9.436662931810237964, -51.82303673229489505 ) ) ;
#155636=ADVANCED_FACE ( 'NONE', ( #79469 ), #102874, .F. ) ;
#155683=EDGE_LOOP ( 'NONE', ( #220477, #125168, #4232, #79769 ) ) ;
#155758=CARTESIAN_POINT ( 'NONE',  ( -16.92209698673480744, 9.950000000011138823, -54.28936443294811198 ) ) ;
#155771=LINE ( 'NONE', #56599, #207412 ) ;
#155895=AXIS2_PLACEMENT_3D ( 'NONE', #128908, #29831, #109314 ) ;
#155992=DIRECTION ( 'NONE',  ( 1.073024830501117725E-15, 0.000000000000000000, 1.000000000000000000 ) ) ;
#156010=ORIENTED_EDGE ( 'NONE', *, *, #198342, .F. ) ;
#156033=CARTESIAN_POINT ( 'NONE',  ( -18.40000000000000213, 5.650000000011139001, -54.35000000000000142 ) ) ;
#156088=CARTESIAN_POINT ( 'NONE',  ( -16.77431908686106610, 9.945805754529134290, -46.16416078234976084 ) ) ;
#156257=CARTESIAN_POINT ( 'NONE',  ( 20.73486653747088937, 7.750000000011182166, -46.15000000000000568 ) ) ;
#156513=ORIENTED_EDGE ( 'NONE', *, *, #4237, .F. ) ;
#156645=EDGE_CURVE ( 'NONE', #27482, #168945, #57375, .T. ) ;
#156729=ORIENTED_EDGE ( 'NONE', *, *, #130520, .F. ) ;
#156781=CARTESIAN_POINT ( 'NONE',  ( -12.33960340485503870, 9.360749169926263491, -50.81457014060730160 ) ) ;
#156853=LINE ( 'NONE', #137251, #226664 ) ;
#156916=LINE ( 'NONE', #59027, #101968 ) ;
#157155=B_SPLINE_CURVE_WITH_KNOTS ( 'NONE', 3,
 ( #162860, #44187, #24642, #239820, #182416, #83266, #139398, #104122, #181134, #179850 ),
 .UNSPECIFIED., .F., .F.,
 ( 4, 3, 3, 4 ),
 ( 1.894194122894209342E-15, 3.877043166999724264E-05, 7.336897548476889550E-05, 7.659383120240112811E-05 ),
 .UNSPECIFIED. ) ;
#157165=B_SPLINE_CURVE_WITH_KNOTS ( 'NONE', 3,
 ( #157922, #34113, #117470, #138281, #35394, #39234, #217819, #58738, #37946, #53637, #152769, #74530, #114895 ),
 .UNSPECIFIED., .F., .F.,
 ( 4, 3, 3, 3, 4 ),
 ( -3.224855718277970714E-06, 0.000000000000000000, 6.199515528665968749E-06, 4.034952380127321888E-05, 7.452715123699268278E-05 ),
 .UNSPECIFIED. ) ;
#157249=EDGE_CURVE ( 'NONE', #222258, #128354, #26972, .T. ) ;
#157371=CARTESIAN_POINT ( 'NONE',  ( -16.87333278164147288, 9.882609784589883262, -46.63316780615359392 ) ) ;
#157468=DIRECTION ( 'NONE',  ( -0.000000000000000000, 1.000000000000000000, -0.000000000000000000 ) ) ;
#157613=LINE ( 'NONE', #58440, #64603 ) ;
#157724=VECTOR ( 'NONE', #150392, 1000.000000000000000 ) ;
#157769=CARTESIAN_POINT ( 'NONE',  ( 20.04999999999999716, 8.750000000011173285, -46.15000000000000568 ) ) ;
#157922=CARTESIAN_POINT ( 'NONE',  ( -16.94445028196807002, 9.992063609708893068, -54.39266982158155628 ) ) ;
#158087=CARTESIAN_POINT ( 'NONE',  ( -15.75000000000000355, 9.350000000011139178, -50.36426760761608534 ) ) ;
#158114=ADVANCED_FACE ( 'NONE', ( #233411 ), #141521, .T. ) ;
#158653=ADVANCED_FACE ( 'NONE', ( #220151 ), #141877, .F. ) ;
#158726=DIRECTION ( 'NONE',  ( -1.000000000000000000, 0.000000000000000000, 0.000000000000000000 ) ) ;
#159269=CARTESIAN_POINT ( 'NONE',  ( -17.78241384941079062, 10.85557575279146469, -43.74903767243881703 ) ) ;
#159376=DIRECTION ( 'NONE',  ( -0.7071067811865487940, 0.7071067811865463515, 0.000000000000000000 ) ) ;
#159394=EDGE_CURVE ( 'NONE', #109277, #191054, #182043, .T. ) ;
#159417=ORIENTED_EDGE ( 'NONE', *, *, #32555, .T. ) ;
#159638=CARTESIAN_POINT ( 'NONE',  ( -20.65000000000000568, 5.650000000011139001, -46.15000000000000568 ) ) ;
#159807=DIRECTION ( 'NONE',  ( -1.000000000000000000, 0.000000000000000000, 0.000000000000000000 ) ) ;
#159942=ADVANCED_FACE ( 'NONE', ( #16558 ), #9776, .F. ) ;
#159953=VECTOR ( 'NONE', #75191, 1000.000000000000000 ) ;
#159956=CYLINDRICAL_SURFACE ( 'NONE', #234104, 1.749999999999998002 ) ;
#159995=PLANE ( 'NONE',  #204102 ) ;
#160147=CARTESIAN_POINT ( 'NONE',  ( -16.93234230245721861, 9.998107370558241058, -54.41769028166626043 ) ) ;
#160496=ORIENTED_EDGE ( 'NONE', *, *, #130520, .T. ) ;
#160700=CARTESIAN_POINT ( 'NONE',  ( -16.79363873026997922, 9.948850229429586634, -54.34615378144547293 ) ) ;
#160711=AXIS2_PLACEMENT_3D ( 'NONE', #110684, #250196, #88530 ) ;
#160873=AXIS2_PLACEMENT_3D ( 'NONE', #211189, #30015, #191663 ) ;
#161011=CARTESIAN_POINT ( 'NONE',  ( -16.86337532320260735, 9.979967204235514089, -54.44892446898280980 ) ) ;
#161083=LINE ( 'NONE', #21575, #219283 ) ;
#161086=CARTESIAN_POINT ( 'NONE',  ( -17.01825945287481545, 9.950000000011138823, -54.25000000000000711 ) ) ;
#161093=VECTOR ( 'NONE', #72060, 1000.000000000000000 ) ;
#161221=EDGE_CURVE ( 'NONE', #212847, #193307, #25586, .T. ) ;
#161243=ORIENTED_EDGE ( 'NONE', *, *, #27033, .F. ) ;
#161266=DIRECTION ( 'NONE',  ( -0.8049926720990042694, -0.5932847527679310229, 0.000000000000000000 ) ) ;
#161327=CARTESIAN_POINT ( 'NONE',  ( -16.27683809663751191, 9.350000000011133849, -42.74999999999997158 ) ) ;
#161439=ORIENTED_EDGE ( 'NONE', *, *, #231318, .F. ) ;
#161647=DIRECTION ( 'NONE',  ( -0.000000000000000000, 1.000000000000000000, -0.000000000000000000 ) ) ;
#161716=LINE ( 'NONE', #140849, #235487 ) ;
#161844=FACE_OUTER_BOUND ( 'NONE', #237218, .T. ) ;
#162013=VECTOR ( 'NONE', #167759, 1000.000000000000000 ) ;
#162154=FACE_BOUND ( 'NONE', #199121, .T. ) ;
#162612=ORIENTED_EDGE ( 'NONE', *, *, #17025, .T. ) ;
#162679=DIRECTION ( 'NONE',  ( 0.000000000000000000, 0.000000000000000000, 1.000000000000000000 ) ) ;
#162860=CARTESIAN_POINT ( 'NONE',  ( -16.89268316805466341, 9.951721813253341153, -46.14424752145445296 ) ) ;
#163110=B_SPLINE_CURVE_WITH_KNOTS ( 'NONE', 3,
 ( #29769, #145813, #225341, #212239, #214778, #153581, #92259, #133952, #15325, #171849, #250064, #72744, #190096, #90980, #173146, #170584, #34900, #113120, #231799 ),
 .UNSPECIFIED., .F., .F.,
 ( 4, 3, 3, 3, 3, 3, 4 ),
 ( 0.0001624081864585774811, 0.0001685232196531728874, 0.0001764526673566831365, 0.0001916878551483135532, 0.0002009890782182522111, 0.0002238845907555150493, 0.0002283406619926365698 ),
 .UNSPECIFIED. ) ;
#163121=CARTESIAN_POINT ( 'NONE',  ( -16.87036670365549540, 9.989418819312804843, -46.02043988269793573 ) ) ;
#163307=ORIENTED_EDGE ( 'NONE', *, *, #184364, .F. ) ;
#163389=CARTESIAN_POINT ( 'NONE',  ( -18.34374000495060386, 11.47316190337362585, -42.74999999999999289 ) ) ;
#163429=CARTESIAN_POINT ( 'NONE',  ( -16.92507428761700439, 9.950000000011138823, -54.28660254037843913 ) ) ;
#163648=CARTESIAN_POINT ( 'NONE',  ( -14.45443560709636976, 9.450592112144857282, -48.55618831880839537 ) ) ;
#163756=VECTOR ( 'NONE', #179354, 1000.000000000000000 ) ;
#163983=CARTESIAN_POINT ( 'NONE',  ( -16.93826681692523550, 10.01142872029886810, -54.44545846735943684 ) ) ;
#164032=ORIENTED_EDGE ( 'NONE', *, *, #32555, .F. ) ;
#164232=CARTESIAN_POINT ( 'NONE',  ( -18.40000000000000213, 11.47316190337362940, -46.10857864376269077 ) ) ;
#164623=EDGE_CURVE ( 'NONE', #197944, #9728, #201326, .T. ) ;
#164644=EDGE_CURVE ( 'NONE', #102761, #100166, #8426, .T. ) ;
#164705=FACE_BOUND ( 'NONE', #129064, .T. ) ;
#164722=DIRECTION ( 'NONE',  ( 0.000000000000000000, 1.000000000000000000, -0.000000000000000000 ) ) ;
#164787=( NAMED_UNIT ( * ) PLANE_ANGLE_UNIT ( ) SI_UNIT ( $, .RADIAN. ) );
#164808=ORIENTED_EDGE ( 'NONE', *, *, #242378, .T. ) ;
#164809=DIRECTION ( 'NONE',  ( 0.000000000000000000, 0.000000000000000000, -1.000000000000000000 ) ) ;
#164867=PLANE ( 'NONE',  #102487 ) ;
#164932=CARTESIAN_POINT ( 'NONE',  ( 12.47034474403012716, 9.375538102059159939, -49.36987588099082558 ) ) ;
#165022=EDGE_CURVE ( 'NONE', #26818, #98813, #251723, .T. ) ;
#165324=EDGE_CURVE ( 'NONE', #71372, #47133, #232340, .T. ) ;
#165407=ORIENTED_EDGE ( 'NONE', *, *, #161221, .T. ) ;
#165537=LINE ( 'NONE', #101657, #171701 ) ;
#165658=VERTEX_POINT ( 'NONE', #41532 ) ;
#165660=CARTESIAN_POINT ( 'NONE',  ( -16.81744102076748959, 9.950000000011138823, -54.35000000000000142 ) ) ;
#165791=ADVANCED_FACE ( 'NONE', ( #188394 ), #201864, .F. ) ;
#165868=DIRECTION ( 'NONE',  ( -0.7071067811865562325, -0.7071067811865388020, 0.000000000000000000 ) ) ;
#166047=LINE ( 'NONE', #60481, #185321 ) ;
#166201=VECTOR ( 'NONE', #168922, 1000.000000000000000 ) ;
#166242=CARTESIAN_POINT ( 'NONE',  ( -13.22483237240078324, 9.436674251854009654, -48.67686193099922320 ) ) ;
#166405=DIRECTION ( 'NONE',  ( -0.000000000000000000, 0.000000000000000000, -1.000000000000000000 ) ) ;
#166468=CARTESIAN_POINT ( 'NONE',  ( -16.79814274880124358, 9.949272542688458287, -46.15243303704799871 ) ) ;
#166733=CARTESIAN_POINT ( 'NONE',  ( -16.87036670365548474, 10.08494996326643189, -54.44999999999999574 ) ) ;
#166880=CARTESIAN_POINT ( 'NONE',  ( -17.78043020864320667, 10.85359211201684637, -56.66304916572023131 ) ) ;
#166893=DIRECTION ( 'NONE',  ( -1.000000000000000000, 0.000000000000000000, 0.000000000000000000 ) ) ;
#167032=FACE_OUTER_BOUND ( 'NONE', #184507, .T. ) ;
#167146=ORIENTED_EDGE ( 'NONE', *, *, #23480, .F. ) ;
#167247=LINE ( 'NONE', #126802, #177295 ) ;
#167283=EDGE_LOOP ( 'NONE', ( #32051, #88800 ) ) ;
#167334=CARTESIAN_POINT ( 'NONE',  ( -23.25000000000000355, 11.75000000001113953, -42.75000000000000000 ) ) ;
#167392=CARTESIAN_POINT ( 'NONE',  ( 13.77030915526558452, 9.456007326080461795, -51.98863349414676094 ) ) ;
#167396=VECTOR ( 'NONE', #147729, 1000.000000000000000 ) ;
#167441=ORIENTED_EDGE ( 'NONE', *, *, #216208, .T. ) ;
#167442=CARTESIAN_POINT ( 'NONE',  ( -14.00000000000000178, 9.850000000011133849, -50.25000000000000711 ) ) ;
#167458=DIRECTION ( 'NONE',  ( 0.000000000000000000, -1.000000000000000000, 0.000000000000000000 ) ) ;
#167734=CYLINDRICAL_SURFACE ( 'NONE', #21954, 0.1000000000000028644 ) ;
#167759=DIRECTION ( 'NONE',  ( 1.186688945009010077E-16, -1.000000000000000000, -0.000000000000000000 ) ) ;
#167842=DIRECTION ( 'NONE',  ( -0.7071067811865463515, -0.7071067811865487940, 7.587431340288849180E-16 ) ) ;
#167864=EDGE_LOOP ( 'NONE', ( #105697, #167441, #5312, #1951 ) ) ;
#168028=EDGE_CURVE ( 'NONE', #43598, #151638, #198100, .T. ) ;
#168252=CARTESIAN_POINT ( 'NONE',  ( -16.97683809663754317, 9.950000000011135270, -53.72847083211058106 ) ) ;
#168323=CARTESIAN_POINT ( 'NONE',  ( -16.89081410710458542, 9.951318529858268036, -54.35440591983636693 ) ) ;
#168574=EDGE_LOOP ( 'NONE', ( #77706, #21444, #257184, #183909, #188692, #203507, #251112, #145516, #151928, #5214, #161243, #156010 ) ) ;
#168644=CARTESIAN_POINT ( 'NONE',  ( -16.83558968593868954, 9.950000000011137047, -54.33769481238329746 ) ) ;
#168694=ADVANCED_FACE ( 'NONE', ( #8585 ), #184641, .F. ) ;
#168752=ORIENTED_EDGE ( 'NONE', *, *, #203269, .F. ) ;
#168922=DIRECTION ( 'NONE',  ( -0.000000000000000000, 1.000000000000000000, 0.000000000000000000 ) ) ;
#168945=VERTEX_POINT ( 'NONE', #233304 ) ;
#168951=APPLICATION_CONTEXT ( 'automotive_design' ) ;
#169050=CARTESIAN_POINT ( 'NONE',  ( -16.87036670365548474, 9.989418819312801290, -54.47956011730205006 ) ) ;
#169303=VERTEX_POINT ( 'NONE', #144415 ) ;
#169406=ORIENTED_EDGE ( 'NONE', *, *, #203529, .T. ) ;
#169536=CARTESIAN_POINT ( 'NONE',  ( -16.94226253665225457, 9.950000000011137047, -54.05326540438422711 ) ) ;
#169743=EDGE_CURVE ( 'NONE', #105073, #192971, #95727, .T. ) ;
#169921=CARTESIAN_POINT ( 'NONE',  ( -16.82542659449980249, 9.934499891438557384, -54.25536439997377869 ) ) ;
#170121=CARTESIAN_POINT ( 'NONE',  ( 13.12220780326572367, 9.430633469083957721, -48.73176579482409210 ) ) ;
#170260=DIRECTION ( 'NONE',  ( 0.000000000000000000, 1.000000000000000000, 0.000000000000000000 ) ) ;
#170584=CARTESIAN_POINT ( 'NONE',  ( -16.93906926870270624, 10.01214687095770906, -46.05345230722682004 ) ) ;
#170898=CARTESIAN_POINT ( 'NONE',  ( -16.89268316805465986, 9.951721813253337601, -54.35575247854554704 ) ) ;
#170985=CARTESIAN_POINT ( 'NONE',  ( -16.80117486205003630, 9.949657268323468529, -54.34885487292548589 ) ) ;
#171701=VECTOR ( 'NONE', #102959, 1000.000000000000000 ) ;
#171843=CARTESIAN_POINT ( 'NONE',  ( 17.74533788810830259, 10.81849979148194763, -43.81362267494758811 ) ) ;
#171849=CARTESIAN_POINT ( 'NONE',  ( -16.93255653858138388, 9.998451453988312920, -46.08164336798968463 ) ) ;
#171884=LINE ( 'NONE', #248827, #184060 ) ;
#171932=EDGE_CURVE ( 'NONE', #145382, #197944, #15657, .T. ) ;
#172080=EDGE_CURVE ( 'NONE', #203380, #182530, #157155, .T. ) ;
#172169=EDGE_CURVE ( 'NONE', #215894, #27850, #42895, .T. ) ;
#172226=DIRECTION ( 'NONE',  ( -0.000000000000000000, 1.000000000000000000, -0.000000000000000000 ) ) ;
#172260=CARTESIAN_POINT ( 'NONE',  ( 20.27550659511088682, 9.216043722520002035, -46.15000000000000568 ) ) ;
#172368=CARTESIAN_POINT ( 'NONE',  ( -20.65000000000000568, 7.250000000011138646, -46.15000000000000568 ) ) ;
#172572=EDGE_LOOP ( 'NONE', ( #137647, #105307, #51598, #21095, #62879, #96229, #145063, #175360, #43139 ) ) ;
#172573=DIRECTION ( 'NONE',  ( -0.000000000000000000, -0.000000000000000000, -1.000000000000000000 ) ) ;
#172739=CARTESIAN_POINT ( 'NONE',  ( -16.89268316805466341, 9.951721813253341153, -46.14424752145445296 ) ) ;
#172838=VECTOR ( 'NONE', #62771, 999.9999999999998863 ) ;
#172968=ORIENTED_EDGE ( 'NONE', *, *, #241128, .T. ) ;
#173053=FACE_OUTER_BOUND ( 'NONE', #172572, .T. ) ;
#173146=CARTESIAN_POINT ( 'NONE',  ( -16.93583594267724024, 10.00862343506335783, -46.05939083932076272 ) ) ;
#173466=CARTESIAN_POINT ( 'NONE',  ( -23.25000000000000355, 11.75000000001113953, -54.35000000000000142 ) ) ;
#173510=EDGE_LOOP ( 'NONE', ( #192772, #68712, #86828, #110157, #78643 ) ) ;
#173539=ORIENTED_EDGE ( 'NONE', *, *, #148122, .T. ) ;
#173552=ORIENTED_EDGE ( 'NONE', *, *, #104147, .T. ) ;
#173884=ORIENTED_EDGE ( 'NONE', *, *, #245442, .F. ) ;
#173952=EDGE_CURVE ( 'NONE', #119072, #40566, #7170, .T. ) ;
#173979=CARTESIAN_POINT ( 'NONE',  ( 15.52844286134408058, 9.375669526436928081, -49.36779000938593498 ) ) ;
#174016=EDGE_LOOP ( 'NONE', ( #125857, #228192, #13855, #100421, #163307 ) ) ;
#174020=ADVANCED_FACE ( 'NONE', ( #179862 ), #85127, .T. ) ;
#174068=DIRECTION ( 'NONE',  ( 1.000000000000000000, -0.000000000000000000, -0.000000000000000000 ) ) ;
#174264=EDGE_CURVE ( 'NONE', #71372, #123899, #244878, .T. ) ;
#174342=CARTESIAN_POINT ( 'NONE',  ( -18.40000000000000213, 5.650000000011139001, -54.35000000000000142 ) ) ;
#174383=CARTESIAN_POINT ( 'NONE',  ( -16.80891096016334529, 9.950000000011137047, -46.13233719273200251 ) ) ;
#174746=DIRECTION ( 'NONE',  ( 0.000000000000000000, 0.000000000000000000, -1.000000000000000000 ) ) ;
#174876=ORIENTED_EDGE ( 'NONE', *, *, #208493, .F. ) ;
#174935=CARTESIAN_POINT ( 'NONE',  ( 20.04999999999999716, 8.750000000011173285, -42.75000000000000000 ) ) ;
#174945=CARTESIAN_POINT ( 'NONE',  ( -16.85312964099708921, 9.913604682078871022, -54.10281570643046223 ) ) ;
#174951=ADVANCED_FACE ( 'NONE', ( #26586 ), #123111, .F. ) ;
#174996=EDGE_LOOP ( 'NONE', ( #229974, #167146, #11507, #141421 ) ) ;
#175083=CARTESIAN_POINT ( 'NONE',  ( -12.68215100488889213, 9.396630376328872103, -51.40705739281828812 ) ) ;
#175214=DIRECTION ( 'NONE',  ( -1.000000000000000000, 0.000000000000000000, 0.000000000000000000 ) ) ;
#175217=DIRECTION ( 'NONE',  ( -0.000000000000000000, -0.000000000000000000, -1.000000000000000000 ) ) ;
#175320=CARTESIAN_POINT ( 'NONE',  ( -17.04295772865528846, 10.02489942527129507, -54.35000000000000853 ) ) ;
#175360=ORIENTED_EDGE ( 'NONE', *, *, #126718, .T. ) ;
#175538=ORIENTED_EDGE ( 'NONE', *, *, #179562, .F. ) ;
#175635=CARTESIAN_POINT ( 'NONE',  ( -16.79270642812324965, 9.946244216949034822, -46.16106672143809675 ) ) ;
#175652=ORIENTED_EDGE ( 'NONE', *, *, #230271, .F. ) ;
#175714=DIRECTION ( 'NONE',  ( 0.000000000000000000, 0.000000000000000000, 1.000000000000000000 ) ) ;
#175720=CARTESIAN_POINT ( 'NONE',  ( -16.89797118371614459, 9.976380722655427746, -46.06270663244127661 ) ) ;
#175924=ORIENTED_EDGE ( 'NONE', *, *, #210309, .F. ) ;
#176016=VECTOR ( 'NONE', #138197, 1000.000000000000000 ) ;
#176081=ORIENTED_EDGE ( 'NONE', *, *, #17025, .F. ) ;
#176192=CARTESIAN_POINT ( 'NONE',  ( -16.87372397896795562, 9.880599536652892922, -53.85072451003576077 ) ) ;
#176209=EDGE_LOOP ( 'NONE', ( #6572, #46182, #181092, #104588 ) ) ;
#176337=CARTESIAN_POINT ( 'NONE',  ( -14.87770893841226716, 9.430637101707896264, -51.76826061806094970 ) ) ;
#176433=CARTESIAN_POINT ( 'NONE',  ( 23.24999999999999645, 8.822561741677553471, -54.34999999999999432 ) ) ;
#176608=CARTESIAN_POINT ( 'NONE',  ( -18.40000000000000213, 8.822561741677553471, -42.75000000000000000 ) ) ;
#176922=ORIENTED_EDGE ( 'NONE', *, *, #137301, .F. ) ;
#176928=CARTESIAN_POINT ( 'NONE',  ( -16.87401514999235275, 9.950000000011137047, -46.21998200746781293 ) ) ;
#177025=CARTESIAN_POINT ( 'NONE',  ( -23.25000000000000355, 5.650000000011139001, -54.35000000000000142 ) ) ;
#177169=CARTESIAN_POINT ( 'NONE',  ( -17.11825945287482753, 10.05000000001113847, -46.14999999999999858 ) ) ;
#177231=CARTESIAN_POINT ( 'NONE',  ( -18.39999999999999858, 11.47867410001043709, -42.77469321634066546 ) ) ;
#177252=LINE ( 'NONE', #114679, #252856 ) ;
#177295=VECTOR ( 'NONE', #65534, 1000.000000000000000 ) ;
#177303=VECTOR ( 'NONE', #172226, 1000.000000000000000 ) ;
#177347=AXIS2_PLACEMENT_3D ( 'NONE', #209322, #129790, #170260 ) ;
#177387=LINE ( 'NONE', #134352, #176016 ) ;
#177511=AXIS2_PLACEMENT_3D ( 'NONE', #257545, #241888, #159807 ) ;
#177649=( NAMED_UNIT ( * ) PLANE_ANGLE_UNIT ( ) SI_UNIT ( $, .RADIAN. ) );
#177942=CYLINDRICAL_SURFACE ( 'NONE', #232359, 0.1999999999999987899 ) ;
#177954=PRODUCT_DEFINITION_FORMATION_WITH_SPECIFIED_SOURCE ( 'ANY', '', #211859, .NOT_KNOWN. ) ;
#178211=CARTESIAN_POINT ( 'NONE',  ( -16.88783316861810135, 9.950000000011137047, -46.25226404197980656 ) ) ;
#178363=PRODUCT_DEFINITION_CONTEXT ( 'detailed design', #137289, 'design' ) ;
#178431=CARTESIAN_POINT ( 'NONE',  ( -16.93860193097148326, 9.993107767340401182, -54.40013836730685881 ) ) ;
#178446=DIRECTION ( 'NONE',  ( 1.652117596168391700E-15, 1.000000000000000000, -0.000000000000000000 ) ) ;
#178494=DIRECTION ( 'NONE',  ( 1.000000000000000000, -0.000000000000000000, -0.000000000000000000 ) ) ;
#178503=B_SPLINE_CURVE_WITH_KNOTS ( 'NONE', 3,
 ( #236283, #94198, #115061, #154235, #156781, #194628, #198441, #36842, #175083, #254535, #75937, #155506, #58901, #18528, #235013, #56346, #96745, #216719, #176337, #78481, #118926, #38104, #139734, #19831, #99318, #117626, #60207, #197150, #158087, #223134 ),
 .UNSPECIFIED., .F., .F.,
 ( 4, 2, 2, 2, 2, 2, 2, 2, 2, 2, 2, 2, 2, 2, 4 ),
 ( 0.000000000000000000, 0.0003422764154113409332, 0.0006845528308226818664, 0.001026829246234022908, 0.001369105661645363733, 0.002053658492468026734, 0.002738211323290689735, 0.003080487738702024272, 0.003422764154113357941, 0.003765040569524692477, 0.004107316984936026580, 0.004449593400347361116, 0.004791869815758694785, 0.005134146231170027587, 0.005476422646581360389 ),
 .UNSPECIFIED. ) ;
#178508=ORIENTED_EDGE ( 'NONE', *, *, #210309, .T. ) ;
#178594=CARTESIAN_POINT ( 'NONE',  ( -17.22767730082241044, 10.34924421247839454, -55.64242869057007113 ) ) ;
#178665=DIRECTION ( 'NONE',  ( 1.073024830501117725E-15, 0.000000000000000000, 1.000000000000000000 ) ) ;
#178784=EDGE_LOOP ( 'NONE', ( #121975, #144669, #229398, #194863 ) ) ;
#178979=LINE ( 'NONE', #82369, #134516 ) ;
#179335=EDGE_LOOP ( 'NONE', ( #99857, #100491 ) ) ;
#179354=DIRECTION ( 'NONE',  ( -0.000000000000000000, -0.000000000000000000, -1.000000000000000000 ) ) ;
#179487=CARTESIAN_POINT ( 'NONE',  ( -16.87683809663752399, 9.850000000011123191, -46.90236401819647938 ) ) ;
#179558=ORIENTED_EDGE ( 'NONE', *, *, #171932, .F. ) ;
#179562=EDGE_CURVE ( 'NONE', #150648, #127380, #14450, .T. ) ;
#179699=CARTESIAN_POINT ( 'NONE',  ( -16.93658211146644987, 9.994108662352344297, -54.40429506995567976 ) ) ;
#179850=CARTESIAN_POINT ( 'NONE',  ( -16.94445028196808778, 9.992063609708889516, -46.10733017841845793 ) ) ;
#179862=FACE_OUTER_BOUND ( 'NONE', #124104, .T. ) ;
#180073=ADVANCED_FACE ( 'NONE', ( #233969 ), #55419, .T. ) ;
#180094=ORIENTED_EDGE ( 'NONE', *, *, #246258, .F. ) ;
#180112=CARTESIAN_POINT ( 'NONE',  ( -17.27223548803219444, 10.34539739140581815, -44.86639382081585836 ) ) ;
#180241=CARTESIAN_POINT ( 'NONE',  ( -16.77828822459933633, 9.946229375067616729, -54.33737174908105771 ) ) ;
#180246=DIRECTION ( 'NONE',  ( -1.000000000000000000, -1.186688945009010077E-16, -0.000000000000000000 ) ) ;
#180282=ORIENTED_EDGE ( 'NONE', *, *, #207320, .T. ) ;
#180385=CARTESIAN_POINT ( 'NONE',  ( -18.37160782347004329, 11.47561641481354044, -42.75000000000000000 ) ) ;
#180469=ORIENTED_EDGE ( 'NONE', *, *, #84734, .T. ) ;
#180476=CARTESIAN_POINT ( 'NONE',  ( -20.65000000000000568, 7.250000000011138646, -42.75000000000000000 ) ) ;
#180781=VERTEX_POINT ( 'NONE', #173466 ) ;
#180887=CIRCLE ( 'NONE', #68460, 14.20833333333333748 ) ;
#181092=ORIENTED_EDGE ( 'NONE', *, *, #815, .T. ) ;
#181134=CARTESIAN_POINT ( 'NONE',  ( -16.94389599338512298, 9.991197989766199328, -46.10764480181025249 ) ) ;
#181828=ORIENTED_EDGE ( 'NONE', *, *, #96077, .F. ) ;
#181986=ORIENTED_EDGE ( 'NONE', *, *, #24997, .F. ) ;
#182043=CIRCLE ( 'NONE', #248675, 1.749999999999998002 ) ;
#182232=AXIS2_PLACEMENT_3D ( 'NONE', #199188, #102613, #201742 ) ;
#182320=CARTESIAN_POINT ( 'NONE',  ( -15.55912972643741199, 8.490870273573719373, -46.04999999999999716 ) ) ;
#182404=PRODUCT_DEFINITION ( 'UNKNOWN', '', #177954, #178363 ) ;
#182416=CARTESIAN_POINT ( 'NONE',  ( -16.92925196614875460, 9.972331796421277872, -46.11674484771679516 ) ) ;
#182443=CARTESIAN_POINT ( 'NONE',  ( -18.40000000000000213, 11.75000000001113953, -46.15000000000000568 ) ) ;
#182530=VERTEX_POINT ( 'NONE', #12490 ) ;
#182586=FACE_OUTER_BOUND ( 'NONE', #102297, .T. ) ;
#182950=CARTESIAN_POINT ( 'NONE',  ( -18.34374000495059676, 11.47316190337362940, -57.75000000000000711 ) ) ;
#183000=CARTESIAN_POINT ( 'NONE',  ( -17.01473183483380680, 9.950000000011138823, -54.25000000000000000 ) ) ;
#183152=DIRECTION ( 'NONE',  ( 0.000000000000000000, -0.000000000000000000, -1.000000000000000000 ) ) ;
#183227=EDGE_CURVE ( 'NONE', #212847, #20798, #183756, .T. ) ;
#183310=LINE ( 'NONE', #2081, #233383 ) ;
#183677=EDGE_LOOP ( 'NONE', ( #150471, #194909, #195200, #12441, #219977, #175538, #99330, #222026, #71595, #18300, #92194, #180282, #48644, #244151 ) ) ;
#183756=LINE ( 'NONE', #25973, #54650 ) ;
#183788=CARTESIAN_POINT ( 'NONE',  ( -14.00000000000000178, 9.850000000011133849, -50.25000000000000711 ) ) ;
#183849=DIRECTION ( 'NONE',  ( -1.000000000000000000, 0.000000000000000000, 0.000000000000000000 ) ) ;
#183909=ORIENTED_EDGE ( 'NONE', *, *, #257151, .T. ) ;
#184060=VECTOR ( 'NONE', #33671, 1000.000000000000000 ) ;
#184162=VECTOR ( 'NONE', #172573, 1000.000000000000000 ) ;
#184211=EDGE_CURVE ( 'NONE', #90311, #26818, #250413, .T. ) ;
#184364=EDGE_CURVE ( 'NONE', #203380, #239517, #124462, .T. ) ;
#184377=DIRECTION ( 'NONE',  ( 0.000000000000000000, -1.000000000000000000, 0.000000000000000000 ) ) ;
#184507=EDGE_LOOP ( 'NONE', ( #196492, #39821, #20189, #30428, #152207, #219208, #154715, #144817, #216029, #253557, #121399, #135224, #37049, #164032 ) ) ;
#184641=PLANE ( 'NONE',  #209195 ) ;
#184703=CARTESIAN_POINT ( 'NONE',  ( -16.87331047859651179, 9.950000000011142376, -46.15000000000000568 ) ) ;
#184864=EDGE_LOOP ( 'NONE', ( #124111, #215202, #178508, #25462, #42813 ) ) ;
#184915=ORIENTED_EDGE ( 'NONE', *, *, #4237, .T. ) ;
#185321=VECTOR ( 'NONE', #140011, 1000.000000000000000 ) ;
#185578=CARTESIAN_POINT ( 'NONE',  ( -16.89155683852559875, 9.950000000011137047, -53.72262815045999673 ) ) ;
#185650=LINE ( 'NONE', #69571, #157724 ) ;
#185763=VECTOR ( 'NONE', #195291, 1000.000000000000000 ) ;
#185773=CARTESIAN_POINT ( 'NONE',  ( -14.56556274378147720, 9.446557523083688679, -48.58994195434590324 ) ) ;
#185780=CARTESIAN_POINT ( 'NONE',  ( 15.06592377766032520, 9.417789466963363054, -48.85738454397687036 ) ) ;
#185828=CARTESIAN_POINT ( 'NONE',  ( -16.83199030136658081, 9.930648033124626295, -46.27240102265748334 ) ) ;
#185999=CARTESIAN_POINT ( 'NONE',  ( -16.78055652883087134, 9.946776916136505164, -46.16079183759243421 ) ) ;
#186028=ORIENTED_EDGE ( 'NONE', *, *, #92662, .T. ) ;
#186353=ADVANCED_FACE ( 'NONE', ( #211258 ), #232120, .F. ) ;
#186417=DIRECTION ( 'NONE',  ( -1.652117596168391700E-15, -1.000000000000000000, 0.000000000000000000 ) ) ;
#186425=ORIENTED_EDGE ( 'NONE', *, *, #67605, .F. ) ;
#186484=ADVANCED_FACE ( 'NONE', ( #53469 ), #93870, .F. ) ;
#186570=CARTESIAN_POINT ( 'NONE',  ( -16.88005004766534967, 9.950100503332199864, -54.35033611194875647 ) ) ;
#186591=ORIENTED_EDGE ( 'NONE', *, *, #197841, .T. ) ;
#186957=CARTESIAN_POINT ( 'NONE',  ( 14.22916352759893144, 9.457410930301314522, -51.99991590874626723 ) ) ;
#187077=CARTESIAN_POINT ( 'NONE',  ( -15.39946565075090135, 9.389534562357855663, -49.17480930438996722 ) ) ;
#187088=CARTESIAN_POINT ( 'NONE',  ( 14.11444803880196552, 9.457431528860066550, -48.49991693789966263 ) ) ;
#187090=CARTESIAN_POINT ( 'NONE',  ( 21.72449340488910252, 10.28395627750227526, -42.75000000000000000 ) ) ;
#187274=EDGE_CURVE ( 'NONE', #120029, #132925, #167247, .T. ) ;
#187615=CARTESIAN_POINT ( 'NONE',  ( 18.54999999999999716, 23.65833333334447985, -50.25000000000000000 ) ) ;
#187655=ADVANCED_FACE ( 'NONE', ( #240195 ), #61550, .F. ) ;
#187926=CARTESIAN_POINT ( 'NONE',  ( 18.54999999999999716, 8.750000000011182166, -42.75000000000000000 ) ) ;
#188006=CARTESIAN_POINT ( 'NONE',  ( -17.04761207306820125, 10.02645087340892971, -46.15000000000000568 ) ) ;
#188350=CARTESIAN_POINT ( 'NONE',  ( 12.25000000000000000, 9.350000000011140955, -50.24999999999999289 ) ) ;
#188378=ORIENTED_EDGE ( 'NONE', *, *, #211308, .T. ) ;
#188394=FACE_OUTER_BOUND ( 'NONE', #184864, .T. ) ;
#188692=ORIENTED_EDGE ( 'NONE', *, *, #195767, .F. ) ;
#189124=CARTESIAN_POINT ( 'NONE',  ( -16.92778301347283687, 10.00094491684646769, -54.42851810796843637 ) ) ;
#189193=CARTESIAN_POINT ( 'NONE',  ( -15.55912972643740488, 8.490870273573721150, -54.35000000000000142 ) ) ;
#189367=VECTOR ( 'NONE', #210803, 1000.000000000000000 ) ;
#189445=CARTESIAN_POINT ( 'NONE',  ( -16.80621392010910142, 9.942202577518921558, -54.31040803458306243 ) ) ;
#189487=EDGE_CURVE ( 'NONE', #152757, #47719, #252736, .T. ) ;
#189539=VECTOR ( 'NONE', #178494, 1000.000000000000000 ) ;
#189768=CARTESIAN_POINT ( 'NONE',  ( -18.38204789744325396, 11.47950103717623982, -57.75000000000000000 ) ) ;
#189934=( BOUNDED_CURVE ( )  B_SPLINE_CURVE ( 3, ( #82561, #183000, #163429, #85128 ),
 .UNSPECIFIED., .F., .F. ) 
 B_SPLINE_CURVE_WITH_KNOTS ( ( 4, 4 ),
 ( 1.570796326794908992, 2.617993877991481533 ),
 .UNSPECIFIED. ) 
 CURVE ( )  GEOMETRIC_REPRESENTATION_ITEM ( )  RATIONAL_B_SPLINE_CURVE ( ( 1.000000000000000000, 0.9106836025229633202, 0.9106836025229633202, 1.000000000000000000 ) ) 
 REPRESENTATION_ITEM ( '' )  );
#190079=DIRECTION ( 'NONE',  ( 0.7071067811865463515, -0.7071067811865487940, 4.930380657631324879E-32 ) ) ;
#190085=CARTESIAN_POINT ( 'NONE',  ( 18.39999999999999503, 11.47316190337363828, -57.75000000000000711 ) ) ;
#190096=CARTESIAN_POINT ( 'NONE',  ( -16.93262454970420094, 10.00202046794151300, -46.07292377376269599 ) ) ;
#190317=AXIS2_PLACEMENT_3D ( 'NONE', #68122, #47249, #248034 ) ;
#190326=ORIENTED_EDGE ( 'NONE', *, *, #34063, .T. ) ;
#190431=CARTESIAN_POINT ( 'NONE',  ( -16.94107738177414291, 10.01423928514777373, -54.44999999999999574 ) ) ;
#190491=CARTESIAN_POINT ( 'NONE',  ( -18.40000000000000213, 5.650000000011139001, -54.35000000000000142 ) ) ;
#190494=DIRECTION ( 'NONE',  ( 0.7071067811865456854, -0.7071067811865493491, -0.000000000000000000 ) ) ;
#190548=CIRCLE ( 'NONE', #132253, 0.1999999999999987899 ) ;
#190804=ADVANCED_FACE ( 'NONE', ( #127407 ), #126098, .F. ) ;
#190823=CARTESIAN_POINT ( 'NONE',  ( 17.23472005113827166, 10.30788195451192379, -55.54657686006867578 ) ) ;
#190918=EDGE_CURVE ( 'NONE', #104591, #90311, #129945, .T. ) ;
#190965=EDGE_CURVE ( 'NONE', #219834, #231063, #185650, .T. ) ;
#191047=CARTESIAN_POINT ( 'NONE',  ( -16.87683809663752399, 9.950000000011142376, -46.15000000000000568 ) ) ;
#191054=VERTEX_POINT ( 'NONE', #68274 ) ;
#191269=CARTESIAN_POINT ( 'NONE',  ( 18.39999999999999503, 5.650000000011139001, -46.15000000000000568 ) ) ;
#191339=ORIENTED_EDGE ( 'NONE', *, *, #194657, .F. ) ;
#191435=CARTESIAN_POINT ( 'NONE',  ( -16.97683809663752186, 9.850000000011137402, -53.59763598180368405 ) ) ;
#191663=DIRECTION ( 'NONE',  ( 0.000000000000000000, 0.000000000000000000, -1.000000000000000000 ) ) ;
#191723=CARTESIAN_POINT ( 'NONE',  ( -16.89797118371569695, 9.976380722655314059, -54.43729336755813364 ) ) ;
#191949=FACE_OUTER_BOUND ( 'NONE', #242468, .T. ) ;
#192085=CARTESIAN_POINT ( 'NONE',  ( 15.57250062127603307, 9.370689921613767126, -51.02646512666105849 ) ) ;
#192100=CARTESIAN_POINT ( 'NONE',  ( 20.05000000000002913, 7.250000000011171508, -42.75000000000000000 ) ) ;
#192125=EDGE_CURVE ( 'NONE', #249345, #50955, #216476, .T. ) ;
#192254=EDGE_CURVE ( 'NONE', #128354, #141210, #119187, .T. ) ;
#192469=ORIENTED_EDGE ( 'NONE', *, *, #24910, .F. ) ;
#192602=EDGE_LOOP ( 'NONE', ( #245707, #36228, #173552, #8545, #145688, #236627, #122683, #243748, #6377 ) ) ;
#192772=ORIENTED_EDGE ( 'NONE', *, *, #125401, .F. ) ;
#192861=CARTESIAN_POINT ( 'NONE',  ( -17.11825945287482753, 9.950000000011131718, -46.15000000000000568 ) ) ;
#192897=ORIENTED_EDGE ( 'NONE', *, *, #79970, .F. ) ;
#192971=VERTEX_POINT ( 'NONE', #62138 ) ;
#193034=LINE ( 'NONE', #96463, #177303 ) ;
#193122=CARTESIAN_POINT ( 'NONE',  ( -21.65000000000000213, 9.950000000011140600, -54.25000000000000711 ) ) ;
#193307=VERTEX_POINT ( 'NONE', #256099 ) ;
#193352=( BOUNDED_CURVE ( )  B_SPLINE_CURVE ( 3, ( #238997, #241554, #60337, #139867 ),
 .UNSPECIFIED., .F., .F. ) 
 B_SPLINE_CURVE_WITH_KNOTS ( ( 4, 4 ),
 ( 3.752122642744676995, 4.712388980384671910 ),
 .UNSPECIFIED. ) 
 CURVE ( )  GEOMETRIC_REPRESENTATION_ITEM ( )  RATIONAL_B_SPLINE_CURVE ( ( 1.000000000000000000, 0.9246222802177364031, 0.9246222802177364031, 1.000000000000000000 ) ) 
 REPRESENTATION_ITEM ( '' )  );
#193762=VECTOR ( 'NONE', #220289, 1000.000000000000000 ) ;
#194628=CARTESIAN_POINT ( 'NONE',  ( -12.42749937872396515, 9.370689921613768902, -51.02646512666106560 ) ) ;
#194657=EDGE_CURVE ( 'NONE', #63272, #90311, #171884, .T. ) ;
#194749=ADVANCED_FACE ( 'NONE', ( #34937 ), #143783, .T. ) ;
#194863=ORIENTED_EDGE ( 'NONE', *, *, #82690, .T. ) ;
#194902=AXIS2_PLACEMENT_3D ( 'NONE', #242942, #241668, #223371 ) ;
#194909=ORIENTED_EDGE ( 'NONE', *, *, #60456, .F. ) ;
#195083=VECTOR ( 'NONE', #175214, 1000.000000000000000 ) ;
#195088=ORIENTED_EDGE ( 'NONE', *, *, #208493, .T. ) ;
#195200=ORIENTED_EDGE ( 'NONE', *, *, #173952, .F. ) ;
#195209=CARTESIAN_POINT ( 'NONE',  ( -16.84981964351502626, 9.917318234110023667, -46.36960161401952263 ) ) ;
#195291=DIRECTION ( 'NONE',  ( -1.000000000000000000, -0.000000000000000000, -0.000000000000000000 ) ) ;
#195649=CARTESIAN_POINT ( 'NONE',  ( 20.99999999999999645, 9.750000000011137757, -46.15000000000000568 ) ) ;
#195761=CARTESIAN_POINT ( 'NONE',  ( -16.81931177881022776, 9.936996059515061930, -54.27321787861723834 ) ) ;
#195767=EDGE_CURVE ( 'NONE', #228728, #243879, #178979, .T. ) ;
#196324=ORIENTED_EDGE ( 'NONE', *, *, #100253, .T. ) ;
#196478=DIRECTION ( 'NONE',  ( 1.186688945009010077E-16, -1.000000000000000000, -0.000000000000000000 ) ) ;
#196492=ORIENTED_EDGE ( 'NONE', *, *, #187274, .F. ) ;
#196517=DIRECTION ( 'NONE',  ( 0.5932847527679310229, -0.8049926720990042694, 0.000000000000000000 ) ) ;
#196527=CARTESIAN_POINT ( 'NONE',  ( -17.11825945287481332, 10.05000000001113847, -54.25000000000000000 ) ) ;
#196628=CARTESIAN_POINT ( 'NONE',  ( -21.65000000000000213, 9.950000000011140600, -46.15000000000000568 ) ) ;
#196652=CARTESIAN_POINT ( 'NONE',  ( 22.88900146558018989, 8.703904791123973084, -54.34999999999999432 ) ) ;
#196686=CARTESIAN_POINT ( 'NONE',  ( -16.97092634996683813, 10.00088896635997315, -46.13014276629746746 ) ) ;
#196832=VERTEX_POINT ( 'NONE', #176433 ) ;
#196898=( GEOMETRIC_REPRESENTATION_CONTEXT ( 3 ) GLOBAL_UNCERTAINTY_ASSIGNED_CONTEXT ( ( #257884 ) ) GLOBAL_UNIT_ASSIGNED_CONTEXT ( ( #223454, #164787, #44835 ) ) REPRESENTATION_CONTEXT ( 'NONE', 'WORKASPACE' ) );
#197002=ORIENTED_EDGE ( 'NONE', *, *, #24475, .T. ) ;
#197150=CARTESIAN_POINT ( 'NONE',  ( -15.73854595235691178, 9.351413679112543065, -50.48034356754896379 ) ) ;
#197312=CARTESIAN_POINT ( 'NONE',  ( -16.97683809663752186, 9.950000000011138823, -46.90236401819648648 ) ) ;
#197437=AXIS2_PLACEMENT_3D ( 'NONE', #1872, #46158, #184377 ) ;
#197814=CARTESIAN_POINT ( 'NONE',  ( -16.87036670365549895, 9.989418819312803066, -46.02043988269794283 ) ) ;
#197841=EDGE_CURVE ( 'NONE', #149877, #248438, #156916, .T. ) ;
#197855=DIRECTION ( 'NONE',  ( 1.186688945009009831E-16, -1.000000000000000000, 0.000000000000000000 ) ) ;
#197944=VERTEX_POINT ( 'NONE', #139868 ) ;
#197948=AXIS2_PLACEMENT_3D ( 'NONE', #150022, #110872, #71767 ) ;
#198100=LINE ( 'NONE', #122428, #154891 ) ;
#198256=( BOUNDED_CURVE ( )  B_SPLINE_CURVE ( 3, ( #209828, #166880, #27377, #248960 ),
 .UNSPECIFIED., .F., .T. ) 
 B_SPLINE_CURVE_WITH_KNOTS ( ( 4, 4 ),
 ( 5.733388419619901200, 5.983100554402348337 ),
 .UNSPECIFIED. ) 
 CURVE ( )  GEOMETRIC_REPRESENTATION_ITEM ( )  RATIONAL_B_SPLINE_CURVE ( ( 1.000000000000000000, 0.9948104011409416580, 0.9948104011409416580, 1.000000000000000000 ) ) 
 REPRESENTATION_ITEM ( '' )  );
#198295=CARTESIAN_POINT ( 'NONE',  ( -16.83199318825828428, 9.930646127992318384, -54.22758518820919704 ) ) ;
#198342=EDGE_CURVE ( 'NONE', #215461, #21223, #1195, .T. ) ;
#198441=CARTESIAN_POINT ( 'NONE',  ( -12.48127053791144903, 9.376580978055098825, -51.12694624701194357 ) ) ;
#198623=DIRECTION ( 'NONE',  ( -1.000000000000000000, 0.000000000000000000, 0.000000000000000000 ) ) ;
#198675=DIRECTION ( 'NONE',  ( 1.000000000000000000, 0.000000000000000000, 0.000000000000000000 ) ) ;
#198863=EDGE_CURVE ( 'NONE', #201931, #227367, #149946, .T. ) ;
#198888=CARTESIAN_POINT ( 'NONE',  ( -16.98495255085919098, 10.00556436600592924, -46.13461720622050422 ) ) ;
#198951=CARTESIAN_POINT ( 'NONE',  ( 15.48841904831874849, 8.561580951692381092, -54.35000000000000853 ) ) ;
#199098=AXIS2_PLACEMENT_3D ( 'NONE', #229896, #207790, #31731 ) ;
#199121=EDGE_LOOP ( 'NONE', ( #202065, #67241 ) ) ;
#199188=CARTESIAN_POINT ( 'NONE',  ( 13.99999999999999822, 9.850000000011137402, -50.24999999999999289 ) ) ;
#199259=CARTESIAN_POINT ( 'NONE',  ( -16.93262454970419384, 10.00202046794151478, -54.42707622623731112 ) ) ;
#199315=DIRECTION ( 'NONE',  ( 0.000000000000000000, 1.000000000000000000, -0.000000000000000000 ) ) ;
#199432=VECTOR ( 'NONE', #174068, 1000.000000000000000 ) ;
#199499=ORIENTED_EDGE ( 'NONE', *, *, #192254, .T. ) ;
#199611=CARTESIAN_POINT ( 'NONE',  ( -16.78493211734302903, 9.945835743215324598, -54.33605098089597618 ) ) ;
#199660=CARTESIAN_POINT ( 'NONE',  ( -16.77683809663752257, 9.945835743215301505, -46.16394901910421567 ) ) ;
#199683=EDGE_CURVE ( 'NONE', #155114, #249345, #213576, .T. ) ;
#199685=CARTESIAN_POINT ( 'NONE',  ( -18.44085059012131822, 11.51401249349495437, -42.75969468087846792 ) ) ;
#199814=VECTOR ( 'NONE', #199315, 1000.000000000000000 ) ;
#199815=CARTESIAN_POINT ( 'NONE',  ( -16.77683809663752257, 9.945835743215303282, -54.33605098089579855 ) ) ;
#199942=ORIENTED_EDGE ( 'NONE', *, *, #159394, .F. ) ;
#199984=AXIS2_PLACEMENT_3D ( 'NONE', #251950, #65306, #143558 ) ;
#199985=VERTEX_POINT ( 'NONE', #169050 ) ;
#200302=CARTESIAN_POINT ( 'NONE',  ( 20.05000000000002913, 7.250000000011171508, -54.35000000000000142 ) ) ;
#200349=ADVANCED_FACE ( 'NONE', ( #124461 ), #164867, .T. ) ;
#200573=DIRECTION ( 'NONE',  ( -1.000000000000000000, 0.000000000000000000, -1.020425574104004196E-15 ) ) ;
#200682=ORIENTED_EDGE ( 'NONE', *, *, #119576, .F. ) ;
#200777=CARTESIAN_POINT ( 'NONE',  ( -18.40000000000000213, 11.47316190337362762, -46.04999999999999716 ) ) ;
#201163=CIRCLE ( 'NONE', #5330, 0.9000000000000014655 ) ;
#201263=CARTESIAN_POINT ( 'NONE',  ( -17.11825945287481332, 10.05000000001113847, -54.35000000000000142 ) ) ;
#201326=B_SPLINE_CURVE_WITH_KNOTS ( 'NONE', 3,
 ( #205312, #44982, #245751, #7118, #187077, #22874, #106211, #222294, #84049, #185773, #163648, #201470, #63244, #206619, #4551, #142769, #86636, #166242, #64536, #28013, #67109, #121952, #123233, #102345, #204043, #107510 ),
 .UNSPECIFIED., .F., .F.,
 ( 4, 2, 2, 2, 2, 2, 2, 2, 2, 2, 2, 2, 4 ),
 ( 0.005476422646581360389, 0.006160811967703580874, 0.006845201288825802227, 0.007187395949386906832, 0.007529590609948009702, 0.007871785270509114307, 0.008213979931070217178, 0.008556174591631321782, 0.008898369252192424653, 0.009240563912753529258, 0.009582758573314632128, 0.01026714789443683960, 0.01095153721555904708 ),
 .UNSPECIFIED. ) ;
#201422=CARTESIAN_POINT ( 'NONE',  ( 23.24999999999999645, 5.650000000011139001, -46.15000000000001279 ) ) ;
#201470=CARTESIAN_POINT ( 'NONE',  ( -14.23072895065543086, 9.455987233623892152, -48.51153116689782507 ) ) ;
#201483=PLANE ( 'NONE',  #106336 ) ;
#201522=DIRECTION ( 'NONE',  ( 0.7071067811865463515, 0.7071067811865487940, 7.587431340288849180E-16 ) ) ;
#201711=CARTESIAN_POINT ( 'NONE',  ( -14.00000000000000178, 9.850000000011133849, -50.25000000000000711 ) ) ;
#201742=DIRECTION ( 'NONE',  ( 1.000000000000000000, 0.000000000000000000, 0.000000000000000000 ) ) ;
#201864=CYLINDRICAL_SURFACE ( 'NONE', #251015, 0.1000000000000001443 ) ;
#201931=VERTEX_POINT ( 'NONE', #119815 ) ;
#202065=ORIENTED_EDGE ( 'NONE', *, *, #94052, .T. ) ;
#202515=EDGE_CURVE ( 'NONE', #144797, #47719, #211872, .T. ) ;
#202585=ORIENTED_EDGE ( 'NONE', *, *, #254764, .F. ) ;
#202701=STYLED_ITEM ( 'NONE', ( #211615 ), #76170 ) ;
#202836=DIRECTION ( 'NONE',  ( 0.000000000000000000, -1.000000000000000000, 0.000000000000000000 ) ) ;
#203022=FACE_OUTER_BOUND ( 'NONE', #116904, .T. ) ;
#203071=DIRECTION ( 'NONE',  ( -1.000000000000000000, 0.000000000000000000, 0.000000000000000000 ) ) ;
#203269=EDGE_CURVE ( 'NONE', #27850, #131288, #150718, .T. ) ;
#203380=VERTEX_POINT ( 'NONE', #120846 ) ;
#203439=EDGE_LOOP ( 'NONE', ( #190326, #87611, #203734, #51461, #100032 ) ) ;
#203507=ORIENTED_EDGE ( 'NONE', *, *, #92662, .F. ) ;
#203526=CIRCLE ( 'NONE', #12004, 0.09999999999999939493 ) ;
#203529=EDGE_CURVE ( 'NONE', #199985, #21668, #42479, .T. ) ;
#203734=ORIENTED_EDGE ( 'NONE', *, *, #165022, .F. ) ;
#203874=EDGE_CURVE ( 'NONE', #98813, #123176, #106045, .T. ) ;
#204040=DIRECTION ( 'NONE',  ( -0.000000000000000000, -0.000000000000000000, -1.000000000000000000 ) ) ;
#204043=CARTESIAN_POINT ( 'NONE',  ( -12.25000000000000533, 9.350000000011133849, -50.01856895740264264 ) ) ;
#204102=AXIS2_PLACEMENT_3D ( 'NONE', #216075, #161266, #196517 ) ;
#204271=FACE_OUTER_BOUND ( 'NONE', #246543, .T. ) ;
#204682=ORIENTED_EDGE ( 'NONE', *, *, #331, .T. ) ;
#204762=ORIENTED_EDGE ( 'NONE', *, *, #44905, .T. ) ;
#205121=CARTESIAN_POINT ( 'NONE',  ( -16.87683809663752399, 9.865889849343641771, -53.73257319293013978 ) ) ;
#205312=CARTESIAN_POINT ( 'NONE',  ( -15.75000000000000355, 9.350000000011140955, -50.25000000000000711 ) ) ;
#205321=CARTESIAN_POINT ( 'NONE',  ( 13.76927104934457269, 9.455987233623899257, -48.51153116689782507 ) ) ;
#205364=AXIS2_PLACEMENT_3D ( 'NONE', #242443, #63828, #41709 ) ;
#205374=CARTESIAN_POINT ( 'NONE',  ( -18.40000000000000213, 11.33174054713633261, -54.35000000000000142 ) ) ;
#205375=CARTESIAN_POINT ( 'NONE',  ( -16.77683809663752257, 9.945835743215301505, -46.16394901910421567 ) ) ;
#205541=CARTESIAN_POINT ( 'NONE',  ( -16.81744102076749314, 9.950000000011142376, -46.15000000000000568 ) ) ;
#205635=DIRECTION ( 'NONE',  ( -1.186688945009010077E-16, 1.000000000000000000, 0.000000000000000000 ) ) ;
#206264=FACE_OUTER_BOUND ( 'NONE', #203439, .T. ) ;
#206413=FACE_OUTER_BOUND ( 'NONE', #27418, .T. ) ;
#206448=CIRCLE ( 'NONE', #60679, 0.9000000000000014655 ) ;
#206451=CARTESIAN_POINT ( 'NONE',  ( -17.11825945287481332, 9.950000000011138823, -54.25000000000000711 ) ) ;
#206619=CARTESIAN_POINT ( 'NONE',  ( -13.88555196119804158, 9.457431528860068326, -48.49991693789967684 ) ) ;
#206739=ORIENTED_EDGE ( 'NONE', *, *, #110923, .F. ) ;
#207073=ORIENTED_EDGE ( 'NONE', *, *, #27128, .F. ) ;
#207286=PLANE ( 'NONE',  #118278 ) ;
#207320=EDGE_CURVE ( 'NONE', #216000, #253186, #165537, .T. ) ;
#207381=CARTESIAN_POINT ( 'NONE',  ( -16.87036670365549895, 10.08494996326643189, -46.04999999999999716 ) ) ;
#207412=VECTOR ( 'NONE', #136141, 1000.000000000000000 ) ;
#207552=EDGE_CURVE ( 'NONE', #127380, #67166, #13635, .T. ) ;
#207790=DIRECTION ( 'NONE',  ( -1.646408749285562691E-14, 1.000000000000000000, 0.000000000000000000 ) ) ;
#207936=CARTESIAN_POINT ( 'NONE',  ( 13.88302573338719093, 9.457410944778569473, -48.50008397379001934 ) ) ;
#208138=EDGE_CURVE ( 'NONE', #129130, #182530, #238994, .T. ) ;
#208297=PLANE ( 'NONE',  #119773 ) ;
#208493=EDGE_CURVE ( 'NONE', #98813, #100166, #230678, .T. ) ;
#208996=CARTESIAN_POINT ( 'NONE',  ( -16.85722902420154412, 9.950000000011138823, -54.23445252622962443 ) ) ;
#209062=DIRECTION ( 'NONE',  ( -1.000000000000000000, 0.000000000000000000, 0.000000000000000000 ) ) ;
#209082=EDGE_LOOP ( 'NONE', ( #106811, #28649, #223294, #247703 ) ) ;
#209195=AXIS2_PLACEMENT_3D ( 'NONE', #124684, #47689, #166405 ) ;
#209293=CARTESIAN_POINT ( 'NONE',  ( -15.75000000000000355, 9.850000000011133849, -50.25000000000000711 ) ) ;
#209322=CARTESIAN_POINT ( 'NONE',  ( -16.77683809663752257, 23.65833333334447985, -50.25000000000000000 ) ) ;
#209522=CARTESIAN_POINT ( 'NONE',  ( 18.39999999999999503, 11.47316190337363828, -46.15000000000000568 ) ) ;
#209646=CARTESIAN_POINT ( 'NONE',  ( 16.87683809663750267, 9.950000000011138823, -46.15000000000000568 ) ) ;
#209828=CARTESIAN_POINT ( 'NONE',  ( -18.40000000000000213, 11.47316190337364183, -57.67405393319205587 ) ) ;
#209887=AXIS2_PLACEMENT_3D ( 'NONE', #183788, #62561, #1277 ) ;
#210296=CARTESIAN_POINT ( 'NONE',  ( -16.89935556175728237, 9.950000000011009149, -53.86032363711485971 ) ) ;
#210309=EDGE_CURVE ( 'NONE', #182530, #73622, #163110, .T. ) ;
#210327=CARTESIAN_POINT ( 'NONE',  ( -18.40000000000000213, 11.48667500176882328, -42.75000000000000000 ) ) ;
#210396=CARTESIAN_POINT ( 'NONE',  ( 20.27550659511089037, 9.216043722520002035, -54.35000000000000142 ) ) ;
#210613=CARTESIAN_POINT ( 'NONE',  ( -18.40000000000000213, 11.48667500176882861, -57.75000000000000000 ) ) ;
#210803=DIRECTION ( 'NONE',  ( -0.000000000000000000, 1.000000000000000000, -0.000000000000000000 ) ) ;
#211158=CARTESIAN_POINT ( 'NONE',  ( -18.34374000495060386, 11.47316190337362585, -42.74999999999999289 ) ) ;
#211189=CARTESIAN_POINT ( 'NONE',  ( -16.27683809663750480, 9.350000000011133849, -42.75000000000000000 ) ) ;
#211258=FACE_OUTER_BOUND ( 'NONE', #106477, .T. ) ;
#211308=EDGE_CURVE ( 'NONE', #230747, #215461, #113158, .T. ) ;
#211575=CARTESIAN_POINT ( 'NONE',  ( -16.77180007708460607, 9.950000000011137047, -54.36438588104517322 ) ) ;
#211615=PRESENTATION_STYLE_ASSIGNMENT (( #132071 ) ) ;
#211649=CARTESIAN_POINT ( 'NONE',  ( 16.87683809663749557, 9.950000000011131718, -54.35000000000000142 ) ) ;
#211774=ORIENTED_EDGE ( 'NONE', *, *, #156645, .T. ) ;
#211828=CARTESIAN_POINT ( 'NONE',  ( -16.87851181299898684, 9.950042924018893231, -46.14985648463308365 ) ) ;
#211859=PRODUCT ( 'Snap Open Cable Crossbars 2', 'Snap Open Cable Crossbars 2', '', ( #11844 ) ) ;
#211862=EDGE_LOOP ( 'NONE', ( #168752, #202585, #174876, #226580, #76673 ) ) ;
#211872=LINE ( 'NONE', #13652, #166201 ) ;
#212239=CARTESIAN_POINT ( 'NONE',  ( -16.94062896051973865, 9.992719105111833144, -46.10251654211879924 ) ) ;
#212476=CARTESIAN_POINT ( 'NONE',  ( -33.72168855820451938, 9.950000000011156587, -54.35000000000005826 ) ) ;
#212554=CARTESIAN_POINT ( 'NONE',  ( -16.92973740335360233, 9.992503814478528312, -54.40605903520227571 ) ) ;
#212847=VERTEX_POINT ( 'NONE', #144041 ) ;
#213081=CARTESIAN_POINT ( 'NONE',  ( -16.94107738177414291, 10.01423928514777373, -54.44999999999999574 ) ) ;
#213195=EDGE_CURVE ( 'NONE', #222258, #129130, #39558, .T. ) ;
#213405=ADVANCED_FACE ( 'NONE', ( #95342 ), #215285, .T. ) ;
#213453=CARTESIAN_POINT ( 'NONE',  ( -16.87998658237754768, 9.950000000011137047, -46.36363956773774930 ) ) ;
#213576=LINE ( 'NONE', #151054, #77204 ) ;
#213691=CARTESIAN_POINT ( 'NONE',  ( -16.92209698673575957, 9.950000000011138823, -46.21063556705156827 ) ) ;
#214203=CARTESIAN_POINT ( 'NONE',  ( 12.30626653967341255, 9.356790025057037496, -50.70482650861389828 ) ) ;
#214247=ORIENTED_EDGE ( 'NONE', *, *, #3728, .T. ) ;
#214403=CARTESIAN_POINT ( 'NONE',  ( -16.87242674293849731, 9.950000000011138823, -54.35109024637235819 ) ) ;
#214764=FACE_OUTER_BOUND ( 'NONE', #25781, .T. ) ;
#214778=CARTESIAN_POINT ( 'NONE',  ( -16.93909480342659890, 9.993078364812696179, -46.10034701667233037 ) ) ;
#214836=B_SPLINE_CURVE_WITH_KNOTS ( 'NONE', 3,
 ( #240947, #163983, #40205, #238364, #62304, #144374, #199259, #80549, #160147, #141831, #42737, #222636, #179699, #178431, #143105, #122283 ),
 .UNSPECIFIED., .F., .F.,
 ( 4, 3, 3, 3, 3, 4 ),
 ( 0.000000000000000000, 1.810570668010275846E-05, 2.740575833571578222E-05, 4.256816319435761416E-05, 5.213463471025089587E-05, 6.641585710717965742E-05 ),
 .UNSPECIFIED. ) ;
#215202=ORIENTED_EDGE ( 'NONE', *, *, #208138, .T. ) ;
#215285=CYLINDRICAL_SURFACE ( 'NONE', #120080, 1.500000000000001332 ) ;
#215376=ORIENTED_EDGE ( 'NONE', *, *, #190965, .F. ) ;
#215461=VERTEX_POINT ( 'NONE', #130011 ) ;
#215474=AXIS2_PLACEMENT_3D ( 'NONE', #157769, #58593, #80721 ) ;
#215563=CARTESIAN_POINT ( 'NONE',  ( -18.40000000000000213, 5.650000000011139001, -46.15000000000000568 ) ) ;
#215650=CARTESIAN_POINT ( 'NONE',  ( -16.88815647973234135, 9.950832619326892114, -46.14721706332599638 ) ) ;
#215894=VERTEX_POINT ( 'NONE', #149833 ) ;
#216000=VERTEX_POINT ( 'NONE', #57151 ) ;
#216029=ORIENTED_EDGE ( 'NONE', *, *, #192125, .F. ) ;
#216075=CARTESIAN_POINT ( 'NONE',  ( 20.27550659511088682, 9.216043722520002035, -42.75000000000000000 ) ) ;
#216208=EDGE_CURVE ( 'NONE', #155114, #150648, #201163, .T. ) ;
#216476=CIRCLE ( 'NONE', #58243, 0.9000000000000014655 ) ;
#216719=CARTESIAN_POINT ( 'NONE',  ( -14.77538296656414829, 9.436662931810239741, -51.82303673229489505 ) ) ;
#216994=( BOUNDED_CURVE ( )  B_SPLINE_CURVE ( 3, ( #211649, #190823, #73437, #10873 ),
 .UNSPECIFIED., .F., .T. ) 
 B_SPLINE_CURVE_WITH_KNOTS ( ( 4, 4 ),
 ( 3.432212674861196966, 3.693332928900581624 ),
 .UNSPECIFIED. ) 
 CURVE ( )  GEOMETRIC_REPRESENTATION_ITEM ( )  RATIONAL_B_SPLINE_CURVE ( ( 1.000000000000000000, 0.9943260843901261525, 0.9943260843901261525, 1.000000000000000000 ) ) 
 REPRESENTATION_ITEM ( '' )  );
#217409=PLANE ( 'NONE',  #222323 ) ;
#217463=DIRECTION ( 'NONE',  ( 0.000000000000000000, 0.000000000000000000, 1.000000000000000000 ) ) ;
#217470=ORIENTED_EDGE ( 'NONE', *, *, #7037, .T. ) ;
#217525=CARTESIAN_POINT ( 'NONE',  ( -16.91049119928364419, 9.950000000011138823, -46.11827960680916760 ) ) ;
#217534=DIRECTION ( 'NONE',  ( 0.000000000000000000, -1.000000000000000000, 0.000000000000000000 ) ) ;
#217793=LINE ( 'NONE', #1320, #123928 ) ;
#217819=CARTESIAN_POINT ( 'NONE',  ( -16.93935632781549572, 9.984730499736244269, -54.38966074871030543 ) ) ;
#217834=VECTOR ( 'NONE', #209062, 1000.000000000000000 ) ;
#217851=ORIENTED_EDGE ( 'NONE', *, *, #107060, .F. ) ;
#218214=DIRECTION ( 'NONE',  ( 1.186688945009009831E-16, -1.000000000000000000, 0.000000000000000000 ) ) ;
#218233=ORIENTED_EDGE ( 'NONE', *, *, #230271, .T. ) ;
#218240=CARTESIAN_POINT ( 'NONE',  ( -17.01764560440512142, 9.950000000011138823, -54.25000000078541973 ) ) ;
#218571=CARTESIAN_POINT ( 'NONE',  ( -16.85722902420150149, 9.950000000011138823, -46.26554747377067400 ) ) ;
#218742=DIRECTION ( 'NONE',  ( -1.073024830501117725E-15, -0.000000000000000000, -1.000000000000000000 ) ) ;
#218787=VECTOR ( 'NONE', #28700, 999.9999999999998863 ) ;
#218789=AXIS2_PLACEMENT_3D ( 'NONE', #153905, #134264, #174746 ) ;
#219118=ORIENTED_EDGE ( 'NONE', *, *, #88032, .T. ) ;
#219137=EDGE_CURVE ( 'NONE', #129914, #21223, #166047, .T. ) ;
#219203=EDGE_CURVE ( 'NONE', #20798, #180781, #87751, .T. ) ;
#219208=ORIENTED_EDGE ( 'NONE', *, *, #252956, .F. ) ;
#219210=CARTESIAN_POINT ( 'NONE',  ( -16.94107738177415357, 10.01423928514777728, -46.04999999999999716 ) ) ;
#219283=VECTOR ( 'NONE', #204040, 1000.000000000000000 ) ;
#219324=DIRECTION ( 'NONE',  ( 0.000000000000000000, 0.000000000000000000, 1.000000000000000000 ) ) ;
#219430=MECHANICAL_DESIGN_GEOMETRIC_PRESENTATION_REPRESENTATION('',(#202701),#98608);
#219714=DIRECTION ( 'NONE',  ( 0.000000000000000000, 0.000000000000000000, 1.000000000000000000 ) ) ;
#219834=VERTEX_POINT ( 'NONE', #79138 ) ;
#219977=ORIENTED_EDGE ( 'NONE', *, *, #207552, .F. ) ;
#220148=DIRECTION ( 'NONE',  ( 1.186688945009009831E-16, -1.000000000000000000, 0.000000000000000000 ) ) ;
#220151=FACE_OUTER_BOUND ( 'NONE', #45127, .T. ) ;
#220289=DIRECTION ( 'NONE',  ( -1.020425574104004196E-15, -0.000000000000000000, -1.000000000000000000 ) ) ;
#220294=ORIENTED_EDGE ( 'NONE', *, *, #199683, .T. ) ;
#220358=CARTESIAN_POINT ( 'NONE',  ( -18.40000000000000213, 11.47316190337364183, -54.45000000000000284 ) ) ;
#220477=ORIENTED_EDGE ( 'NONE', *, *, #100253, .F. ) ;
#220784=CARTESIAN_POINT ( 'NONE',  ( -18.40000000000000213, 11.48667500176882328, -42.75000000000000000 ) ) ;
#220962=CARTESIAN_POINT ( 'NONE',  ( -16.87036670365548474, 9.989418819312801290, -54.47956011730205006 ) ) ;
#221160=EDGE_CURVE ( 'NONE', #52893, #105073, #230894, .T. ) ;
#221814=LINE ( 'NONE', #43211, #172838 ) ;
#222026=ORIENTED_EDGE ( 'NONE', *, *, #242378, .F. ) ;
#222108=FACE_OUTER_BOUND ( 'NONE', #29305, .T. ) ;
#222258=VERTEX_POINT ( 'NONE', #60945 ) ;
#222294=CARTESIAN_POINT ( 'NONE',  ( -14.87779219673428699, 9.430633469083952392, -48.73176579482408499 ) ) ;
#222323=AXIS2_PLACEMENT_3D ( 'NONE', #201711, #197855, #236999 ) ;
#222333=ORIENTED_EDGE ( 'NONE', *, *, #165324, .T. ) ;
#222499=CARTESIAN_POINT ( 'NONE',  ( 15.07585980824113037, 9.417632963117446465, -51.64894846573224640 ) ) ;
#222636=CARTESIAN_POINT ( 'NONE',  ( -16.93521499325732549, 9.994786119814678571, -54.40710854109355665 ) ) ;
#223134=CARTESIAN_POINT ( 'NONE',  ( -15.75000000000000355, 9.350000000011140955, -50.25000000000000711 ) ) ;
#223294=ORIENTED_EDGE ( 'NONE', *, *, #49861, .T. ) ;
#223371=DIRECTION ( 'NONE',  ( 0.000000000000000000, 0.000000000000000000, -1.000000000000000000 ) ) ;
#223420=SHAPE_REPRESENTATION ( 'Snap Open Cable Crossbars 2', ( #2425 ), #32042 ) ;
#223454=( LENGTH_UNIT ( ) NAMED_UNIT ( * ) SI_UNIT ( .MILLI., .METRE. ) );
#223465=DIRECTION ( 'NONE',  ( -1.020425574104004196E-15, -1.210927747993693964E-31, 1.000000000000000000 ) ) ;
#223492=AXIS2_PLACEMENT_3D ( 'NONE', #223757, #107672, #225033 ) ;
#223524=CARTESIAN_POINT ( 'NONE',  ( -16.88460203013675809, 9.954759003246870463, -54.36589180953823330 ) ) ;
#223757=CARTESIAN_POINT ( 'NONE',  ( 20.73486653747088937, 7.750000000011182166, -54.35000000000000142 ) ) ;
#223855=EDGE_CURVE ( 'NONE', #47133, #192971, #203526, .T. ) ;
#223977=CARTESIAN_POINT ( 'NONE',  ( 18.39999999999999503, 5.650000000011139001, -46.15000000000000568 ) ) ;
#224330=ADVANCED_FACE ( 'NONE', ( #109480 ), #5229, .F. ) ;
#224587=ORIENTED_EDGE ( 'NONE', *, *, #98664, .T. ) ;
#224617=EDGE_CURVE ( 'NONE', #151638, #27482, #19389, .T. ) ;
#224674=DIRECTION ( 'NONE',  ( 0.000000000000000000, 0.000000000000000000, 1.000000000000000000 ) ) ;
#224693=CARTESIAN_POINT ( 'NONE',  ( -16.87683809663752399, 9.950000000011137047, -53.59763598180367694 ) ) ;
#224819=CARTESIAN_POINT ( 'NONE',  ( -23.25000000000000355, 9.950000000011138823, -42.75000000000000000 ) ) ;
#224828=CARTESIAN_POINT ( 'NONE',  ( 23.24999999999999645, 8.822561741677553471, -46.15000000000001279 ) ) ;
#224887=CARTESIAN_POINT ( 'NONE',  ( 13.22261339317536688, 9.436552840015581367, -48.67795547276031698 ) ) ;
#224896=ORIENTED_EDGE ( 'NONE', *, *, #51951, .T. ) ;
#225033=DIRECTION ( 'NONE',  ( 1.000000000000000000, 0.000000000000000000, 0.000000000000000000 ) ) ;
#225035=VERTEX_POINT ( 'NONE', #4305 ) ;
#225098=CARTESIAN_POINT ( 'NONE',  ( -16.77828822508139694, 9.946229374931901290, -46.16262825137395254 ) ) ;
#225108=PLANE ( 'NONE',  #152161 ) ;
#225341=CARTESIAN_POINT ( 'NONE',  ( -16.94180778212363236, 9.992443055743304825, -46.10418357053324456 ) ) ;
#225495=CARTESIAN_POINT ( 'NONE',  ( -21.64999999999999858, 9.350000000011133849, -42.75000000000000000 ) ) ;
#225565=CARTESIAN_POINT ( 'NONE',  ( -16.97683809663752186, 9.850000000011140955, -46.15000000000000568 ) ) ;
#225582=CARTESIAN_POINT ( 'NONE',  ( -16.89021194854739960, 9.950000000011135270, -54.24256813160434376 ) ) ;
#225721=LINE ( 'NONE', #84917, #227445 ) ;
#225723=AXIS2_PLACEMENT_3D ( 'NONE', #233769, #69561, #92953 ) ;
#225936=PLANE ( 'NONE',  #96447 ) ;
#225970=B_SPLINE_CURVE_WITH_KNOTS ( 'NONE', 3,
 ( #111518, #128515, #91946, #189768, #90653, #228900, #210613 ),
 .UNSPECIFIED., .F., .F.,
 ( 4, 3, 4 ),
 ( 0.000000000000000000, 3.882884552234471334E-05, 5.798605692158493495E-05 ),
 .UNSPECIFIED. ) ;
#226073=CARTESIAN_POINT ( 'NONE',  ( -16.97683809663752186, 9.950000000011138823, -46.90236401819648648 ) ) ;
#226196=LINE ( 'NONE', #64579, #243497 ) ;
#226302=CARTESIAN_POINT ( 'NONE',  ( -16.87036670365548474, 9.989418819312801290, -54.47956011730205006 ) ) ;
#226379=CARTESIAN_POINT ( 'NONE',  ( -16.77779411503079032, 9.946101446935278645, -46.16305741761983228 ) ) ;
#226580=ORIENTED_EDGE ( 'NONE', *, *, #118019, .F. ) ;
#226591=ORIENTED_EDGE ( 'NONE', *, *, #137301, .T. ) ;
#226664=VECTOR ( 'NONE', #133413, 1000.000000000000000 ) ;
#227185=CYLINDRICAL_SURFACE ( 'NONE', #190317, 0.5000000000000004441 ) ;
#227367=VERTEX_POINT ( 'NONE', #3608 ) ;
#227445=VECTOR ( 'NONE', #144909, 1000.000000000000000 ) ;
#227462=CARTESIAN_POINT ( 'NONE',  ( 12.29592348164039350, 9.355806591641286474, -49.79110253154616572 ) ) ;
#227516=CARTESIAN_POINT ( 'NONE',  ( -18.40000000000000213, 11.47316190337364183, -54.45000000000000284 ) ) ;
#227533=EDGE_CURVE ( 'NONE', #20990, #253186, #72598, .T. ) ;
#227906=AXIS2_PLACEMENT_3D ( 'NONE', #137998, #217534, #79306 ) ;
#228157=ORIENTED_EDGE ( 'NONE', *, *, #161221, .F. ) ;
#228192=ORIENTED_EDGE ( 'NONE', *, *, #208138, .F. ) ;
#228276=VECTOR ( 'NONE', #28893, 1000.000000000000000 ) ;
#228284=ADVANCED_FACE ( 'NONE', ( #191949 ), #1058, .T. ) ;
#228728=VERTEX_POINT ( 'NONE', #125847 ) ;
#228851=CARTESIAN_POINT ( 'NONE',  ( -16.87845715379269507, 9.957858113908168107, -46.12380065105890026 ) ) ;
#228900=CARTESIAN_POINT ( 'NONE',  ( -18.39418127959864790, 11.48390560170929220, -57.75000000000000000 ) ) ;
#229213=LINE ( 'NONE', #111831, #105080 ) ;
#229281=ORIENTED_EDGE ( 'NONE', *, *, #331, .F. ) ;
#229358=FACE_OUTER_BOUND ( 'NONE', #61573, .T. ) ;
#229398=ORIENTED_EDGE ( 'NONE', *, *, #18515, .F. ) ;
#229448=ORIENTED_EDGE ( 'NONE', *, *, #257839, .T. ) ;
#229472=EDGE_CURVE ( 'NONE', #53148, #20990, #114985, .T. ) ;
#229544=CARTESIAN_POINT ( 'NONE',  ( -16.91256925476569606, 9.985731158139328656, -54.46764248900526439 ) ) ;
#229659=CARTESIAN_POINT ( 'NONE',  ( -17.29158576265544056, 10.36474766602906783, -44.91724175520782580 ) ) ;
#229765=EDGE_LOOP ( 'NONE', ( #152558, #110120, #150000 ) ) ;
#229896=CARTESIAN_POINT ( 'NONE',  ( 20.73486653747088582, 7.250000000011182166, -42.75000000000000000 ) ) ;
#229974=ORIENTED_EDGE ( 'NONE', *, *, #246258, .T. ) ;
#230007=VECTOR ( 'NONE', #112380, 1000.000000000000000 ) ;
#230271=EDGE_CURVE ( 'NONE', #154908, #215461, #35815, .T. ) ;
#230399=EDGE_CURVE ( 'NONE', #253186, #230747, #155771, .T. ) ;
#230549=CARTESIAN_POINT ( 'NONE',  ( -23.25000000000000355, 11.75000000001113953, -42.75000000000000000 ) ) ;
#230678=CIRCLE ( 'NONE', #118230, 0.1000000000000028644 ) ;
#230747=VERTEX_POINT ( 'NONE', #144851 ) ;
#230840=CARTESIAN_POINT ( 'NONE',  ( -16.88853107394619357, 9.950878483358135185, -54.35293634689223552 ) ) ;
#230841=CARTESIAN_POINT ( 'NONE',  ( -16.87036670365548474, 9.989418819312801290, -54.47956011730205006 ) ) ;
#230880=CARTESIAN_POINT ( 'NONE',  ( -18.39999999999999858, 11.47316190337362762, -42.82594606680797256 ) ) ;
#230894=B_SPLINE_CURVE_WITH_KNOTS ( 'NONE', 3,
 ( #205541, #85569, #26956, #166468, #127309, #106431, #185999, #2207, #244673, #225098, #226379, #245979, #4763 ),
 .UNSPECIFIED., .F., .F.,
 ( 4, 3, 3, 3, 4 ),
 ( 1.084999851846394554E-16, 1.946463881814392694E-05, 3.922356109944192040E-05, 4.215060953238614744E-05, 4.415117091093003941E-05 ),
 .UNSPECIFIED. ) ;
#231057=VECTOR ( 'NONE', #96497, 1000.000000000000000 ) ;
#231063=VERTEX_POINT ( 'NONE', #23610 ) ;
#231064=CARTESIAN_POINT ( 'NONE',  ( -17.11825945287482753, 10.05000000001113847, -46.15000000000000568 ) ) ;
#231193=SURFACE_STYLE_FILL_AREA ( #250724 ) ;
#231213=CARTESIAN_POINT ( 'NONE',  ( 15.74999999999998934, 9.350000000011137402, -50.36574316727390510 ) ) ;
#231318=EDGE_CURVE ( 'NONE', #191054, #109277, #140734, .T. ) ;
#231490=ORIENTED_EDGE ( 'NONE', *, *, #145496, .T. ) ;
#231653=CARTESIAN_POINT ( 'NONE',  ( 18.39999999999999503, 8.822561741677553471, -57.75000000000000000 ) ) ;
#231799=CARTESIAN_POINT ( 'NONE',  ( -16.94107738177415712, 10.01423928514777728, -46.04999999999999716 ) ) ;
#231930=CARTESIAN_POINT ( 'NONE',  ( -16.77683809663752257, 23.65833333334447985, -50.25000000000000000 ) ) ;
#231938=LINE ( 'NONE', #196628, #47928 ) ;
#232120=CYLINDRICAL_SURFACE ( 'NONE', #197948, 1.749999999999999778 ) ;
#232121=CARTESIAN_POINT ( 'NONE',  ( -15.75000000000000355, 9.850000000011133849, -50.25000000000000711 ) ) ;
#232267=( BOUNDED_CURVE ( )  B_SPLINE_CURVE ( 3, ( #150960, #171843, #130098, #209646 ),
 .UNSPECIFIED., .F., .T. ) 
 B_SPLINE_CURVE_WITH_KNOTS ( ( 4, 4 ),
 ( 2.589852378279006828, 2.850972632318390154 ),
 .UNSPECIFIED. ) 
 CURVE ( )  GEOMETRIC_REPRESENTATION_ITEM ( )  RATIONAL_B_SPLINE_CURVE ( ( 1.000000000000000000, 0.9943260843901262636, 0.9943260843901262636, 1.000000000000000000 ) ) 
 REPRESENTATION_ITEM ( '' )  );
#232338=CIRCLE ( 'NONE', #99008, 1.749999999999999778 ) ;
#232340=LINE ( 'NONE', #250585, #230007 ) ;
#232359=AXIS2_PLACEMENT_3D ( 'NONE', #257402, #99642, #126945 ) ;
#232394=CARTESIAN_POINT ( 'NONE',  ( -18.40000000000000213, 11.48667500176882861, -57.75000000000000000 ) ) ;
#232500=CARTESIAN_POINT ( 'NONE',  ( 12.48201962039796165, 9.376659938544690931, -51.12819254821728521 ) ) ;
#232515=CARTESIAN_POINT ( 'NONE',  ( -18.40000000000000213, 11.47316190337310893, -57.70017075153427299 ) ) ;
#232941=AXIS2_PLACEMENT_3D ( 'NONE', #225565, #66527, #87346 ) ;
#232945=DIRECTION ( 'NONE',  ( -0.7071067811865456854, 0.7071067811865493491, 0.000000000000000000 ) ) ;
#233304=CARTESIAN_POINT ( 'NONE',  ( -21.65000000000000213, 7.250000000011139534, -54.35000000000000142 ) ) ;
#233383=VECTOR ( 'NONE', #82880, 1000.000000000000000 ) ;
#233411=FACE_OUTER_BOUND ( 'NONE', #174996, .T. ) ;
#233489=CARTESIAN_POINT ( 'NONE',  ( -21.65000000000000213, 7.250000000011138646, -54.35000000000000142 ) ) ;
#233638=ORIENTED_EDGE ( 'NONE', *, *, #42080, .T. ) ;
#233769=CARTESIAN_POINT ( 'NONE',  ( 18.39999999999999503, 5.650000000011139001, -46.15000000000000568 ) ) ;
#233969=FACE_OUTER_BOUND ( 'NONE', #211862, .T. ) ;
#234104=AXIS2_PLACEMENT_3D ( 'NONE', #20441, #196478, #115676 ) ;
#234537=CARTESIAN_POINT ( 'NONE',  ( -16.87242674293850797, 9.950000000011138823, -46.14890975362765602 ) ) ;
#234599=DIRECTION ( 'NONE',  ( 1.000000000000000000, 0.000000000000000000, 0.000000000000000000 ) ) ;
#234791=LINE ( 'NONE', #237362, #4355 ) ;
#234862=ORIENTED_EDGE ( 'NONE', *, *, #257406, .T. ) ;
#235013=CARTESIAN_POINT ( 'NONE',  ( -14.22969084473441370, 9.456007326080463571, -51.98863349414677515 ) ) ;
#235030=SHAPE_REPRESENTATION_RELATIONSHIP ( 'NONE' , 'NONE' ,  #223420, #76170 ) ;
#235230=CARTESIAN_POINT ( 'NONE',  ( -16.87331047859651179, 9.950000000011142376, -46.15000000000000568 ) ) ;
#235402=ADVANCED_FACE ( 'NONE', ( #206264 ), #8071, .F. ) ;
#235487=VECTOR ( 'NONE', #99126, 1000.000000000000000 ) ;
#235533=DIRECTION ( 'NONE',  ( -0.000000000000000000, 1.000000000000000000, -0.000000000000000000 ) ) ;
#235882=LINE ( 'NONE', #117237, #33072 ) ;
#235943=DIRECTION ( 'NONE',  ( 1.186688945009010077E-16, -1.000000000000000000, -0.000000000000000000 ) ) ;
#236142=CARTESIAN_POINT ( 'NONE',  ( -16.87683809663752754, 9.864913447291344895, -53.72428155130396732 ) ) ;
#236283=CARTESIAN_POINT ( 'NONE',  ( -12.25000000000000178, 9.350000000011139178, -50.25000000000000000 ) ) ;
#236338=CARTESIAN_POINT ( 'NONE',  ( -18.40000000000000213, 11.48667500176882861, -57.75000000000000000 ) ) ;
#236627=ORIENTED_EDGE ( 'NONE', *, *, #183227, .F. ) ;
#236863=CARTESIAN_POINT ( 'NONE',  ( -16.82542659449978473, 9.934499891438610675, -46.24463560002602236 ) ) ;
#236999=DIRECTION ( 'NONE',  ( 1.000000000000000000, 1.186688945009009831E-16, 0.000000000000000000 ) ) ;
#237218=EDGE_LOOP ( 'NONE', ( #54270, #43809, #156729, #176081, #101359 ) ) ;
#237240=EDGE_CURVE ( 'NONE', #168945, #123176, #157613, .T. ) ;
#237362=CARTESIAN_POINT ( 'NONE',  ( -20.65000000000000568, 7.250000000011138646, -46.15000000000000568 ) ) ;
#237695=EDGE_CURVE ( 'NONE', #248438, #249345, #206448, .T. ) ;
#238142=CARTESIAN_POINT ( 'NONE',  ( -16.87683809663752754, 9.865889849343568940, -46.76742680706958311 ) ) ;
#238225=CARTESIAN_POINT ( 'NONE',  ( -16.94878442675512886, 9.991729103002159107, -46.11178042436211655 ) ) ;
#238364=CARTESIAN_POINT ( 'NONE',  ( -16.93433913041102912, 10.00597842153509376, -54.43536542739516904 ) ) ;
#238532=CARTESIAN_POINT ( 'NONE',  ( -18.37013991200266005, 11.49974761622313224, -57.79302301051711765 ) ) ;
#238554=DIRECTION ( 'NONE',  ( -1.000000000000000000, 0.000000000000000000, 0.000000000000000000 ) ) ;
#238753=ORIENTED_EDGE ( 'NONE', *, *, #203529, .F. ) ;
#238793=CARTESIAN_POINT ( 'NONE',  ( -17.29838795458562473, 10.37154985795925199, -44.89525871738297980 ) ) ;
#238994=( BOUNDED_CURVE ( )  B_SPLINE_CURVE ( 3, ( #28974, #188006, #198888, #20268 ),
 .UNSPECIFIED., .F., .F. ) 
 B_SPLINE_CURVE_WITH_KNOTS ( ( 4, 4 ),
 ( 4.712388980384689674, 5.672655318024644622 ),
 .UNSPECIFIED. ) 
 CURVE ( )  GEOMETRIC_REPRESENTATION_ITEM ( )  RATIONAL_B_SPLINE_CURVE ( ( 1.000000000000000000, 0.9246222802177426203, 0.9246222802177426203, 1.000000000000000000 ) ) 
 REPRESENTATION_ITEM ( '' )  );
#238997=CARTESIAN_POINT ( 'NONE',  ( -16.94445028196807002, 9.992063609708893068, -54.39266982158155628 ) ) ;
#239118=EDGE_LOOP ( 'NONE', ( #145077, #155061, #218233, #6612, #59836, #130284 ) ) ;
#239182=SURFACE_STYLE_FILL_AREA ( #100905 ) ;
#239378=ORIENTED_EDGE ( 'NONE', *, *, #42080, .F. ) ;
#239404=LINE ( 'NONE', #156033, #69322 ) ;
#239458=ORIENTED_EDGE ( 'NONE', *, *, #190965, .T. ) ;
#239517=VERTEX_POINT ( 'NONE', #184703 ) ;
#239525=CARTESIAN_POINT ( 'NONE',  ( -16.90202395485760078, 9.965944544561997631, -46.09698627874021781 ) ) ;
#239711=DIRECTION ( 'NONE',  ( -1.020425574104004196E-15, 0.000000000000000000, 1.000000000000000000 ) ) ;
#239820=CARTESIAN_POINT ( 'NONE',  ( -16.92132318717937522, 9.966070024017081863, -46.12240663035206722 ) ) ;
#239970=ORIENTED_EDGE ( 'NONE', *, *, #250118, .T. ) ;
#240005=CARTESIAN_POINT ( 'NONE',  ( -16.77683809663752257, 9.945835743215303282, -54.33605098089579855 ) ) ;
#240143=EDGE_CURVE ( 'NONE', #129914, #169303, #1335, .T. ) ;
#240195=FACE_OUTER_BOUND ( 'NONE', #229765, .T. ) ;
#240482=ADVANCED_FACE ( 'NONE', ( #203022 ), #4803, .F. ) ;
#240542=CARTESIAN_POINT ( 'NONE',  ( -16.86578989773640913, 9.984809801269950214, -54.46466488662223782 ) ) ;
#240668=CARTESIAN_POINT ( 'NONE',  ( -16.87683809663753109, 9.864913778549569301, -46.77571563563853374 ) ) ;
#240670=CARTESIAN_POINT ( 'NONE',  ( 16.87683809663750267, 9.950000000011138823, -46.15000000000000568 ) ) ;
#240854=DIRECTION ( 'NONE',  ( -1.020425574104004196E-15, -1.210927747993693964E-31, -1.000000000000000000 ) ) ;
#240947=CARTESIAN_POINT ( 'NONE',  ( -16.94107738177414291, 10.01423928514777373, -54.44999999999999574 ) ) ;
#240991=CARTESIAN_POINT ( 'NONE',  ( 13.99999999999999822, 9.850000000011137402, -50.24999999999999289 ) ) ;
#241069=AXIS2_PLACEMENT_3D ( 'NONE', #187615, #45517, #149778 ) ;
#241128=EDGE_CURVE ( 'NONE', #43598, #212847, #56474, .T. ) ;
#241554=CARTESIAN_POINT ( 'NONE',  ( -16.98495255085918032, 10.00556436600592569, -54.36538279377951000 ) ) ;
#241569=CARTESIAN_POINT ( 'NONE',  ( -17.01825945287482966, 10.05000000001113847, -46.15000000000000568 ) ) ;
#241632=ORIENTED_EDGE ( 'NONE', *, *, #51951, .F. ) ;
#241668=DIRECTION ( 'NONE',  ( 1.000000000000000000, -0.000000000000000000, -0.000000000000000000 ) ) ;
#241731=CARTESIAN_POINT ( 'NONE',  ( -21.65000000000000213, 10.05000000001113847, -54.35000000000000142 ) ) ;
#241833=DIRECTION ( 'NONE',  ( -0.000000000000000000, 1.000000000000000000, -0.000000000000000000 ) ) ;
#241888=DIRECTION ( 'NONE',  ( -1.073024830501117725E-15, -0.000000000000000000, -1.000000000000000000 ) ) ;
#242374=CARTESIAN_POINT ( 'NONE',  ( -17.80356949363865837, 10.87673139701229630, -56.71307302422879815 ) ) ;
#242378=EDGE_CURVE ( 'NONE', #144454, #155114, #12466, .T. ) ;
#242443=CARTESIAN_POINT ( 'NONE',  ( -23.25000000000000355, 5.650000000011139001, -42.75000000000000000 ) ) ;
#242468=EDGE_LOOP ( 'NONE', ( #94268, #105309 ) ) ;
#242942=CARTESIAN_POINT ( 'NONE',  ( -33.72168855820452649, 23.65833333334447985, -50.25000000000000000 ) ) ;
#243047=LINE ( 'NONE', #126962, #10198 ) ;
#243169=DIRECTION ( 'NONE',  ( 1.000000000000000000, 0.000000000000000000, -0.000000000000000000 ) ) ;
#243238=PLANE ( 'NONE',  #38409 ) ;
#243253=CARTESIAN_POINT ( 'NONE',  ( -16.86422026484316916, 9.970447360871808939, -46.08221322567300149 ) ) ;
#243351=EDGE_LOOP ( 'NONE', ( #59558, #104032, #224896, #186591 ) ) ;
#243490=DIRECTION ( 'NONE',  ( 1.000000000000000000, 1.186688945009010077E-16, 0.000000000000000000 ) ) ;
#243497=VECTOR ( 'NONE', #125837, 1000.000000000000000 ) ;
#243748=ORIENTED_EDGE ( 'NONE', *, *, #82690, .F. ) ;
#243879=VERTEX_POINT ( 'NONE', #132827 ) ;
#244151=ORIENTED_EDGE ( 'NONE', *, *, #24910, .T. ) ;
#244673=CARTESIAN_POINT ( 'NONE',  ( -16.77902162784673834, 9.946419257218996890, -46.16199124406934828 ) ) ;
#244859=ORIENTED_EDGE ( 'NONE', *, *, #190918, .T. ) ;
#244878=CIRCLE ( 'NONE', #115713, 0.09999999999999939493 ) ;
#245088=DIRECTION ( 'NONE',  ( -1.000000000000000000, 1.652117596168391700E-15, 0.000000000000000000 ) ) ;
#245128=VECTOR ( 'NONE', #250458, 1000.000000000000000 ) ;
#245183=CARTESIAN_POINT ( 'NONE',  ( -16.84419801905645642, 9.950000000011140600, -54.33051015377797910 ) ) ;
#245219=DIRECTION ( 'NONE',  ( 0.2834754621636439431, -0.2834754621636535465, -0.9161240771326838450 ) ) ;
#245253=CARTESIAN_POINT ( 'NONE',  ( -16.87331047859649757, 9.950000000011138823, -54.35000000000000142 ) ) ;
#245376=CARTESIAN_POINT ( 'NONE',  ( 23.04999999999999716, 8.822561741677553471, -54.34999999999999432 ) ) ;
#245442=EDGE_CURVE ( 'NONE', #193307, #180781, #77877, .T. ) ;
#245467=AXIS2_PLACEMENT_3D ( 'NONE', #166733, #128869, #143276 ) ;
#245707=ORIENTED_EDGE ( 'NONE', *, *, #157249, .F. ) ;
#245717=EDGE_CURVE ( 'NONE', #50955, #91552, #221814, .T. ) ;
#245751=CARTESIAN_POINT ( 'NONE',  ( -15.70407651835961005, 9.355806591641288250, -49.79110253154618704 ) ) ;
#245842=CARTESIAN_POINT ( 'NONE',  ( -16.86337532320262156, 9.979967204235514089, -46.05107553101719020 ) ) ;
#245979=CARTESIAN_POINT ( 'NONE',  ( -16.77732147278574715, 9.945966932584589415, -46.16350875687581379 ) ) ;
#246193=EDGE_CURVE ( 'NONE', #2821, #225035, #25916, .T. ) ;
#246258=EDGE_CURVE ( 'NONE', #104591, #199985, #16510, .T. ) ;
#246543=EDGE_LOOP ( 'NONE', ( #108563, #128038, #109681 ) ) ;
#246545=ADVANCED_FACE ( 'NONE', ( #98663 ), #159995, .F. ) ;
#246631=CARTESIAN_POINT ( 'NONE',  ( -17.22361732159832215, 10.34515565861359221, -44.87078452586714405 ) ) ;
#246887=CARTESIAN_POINT ( 'NONE',  ( 16.27683809663749770, 9.350000000011137402, -42.75000000000000000 ) ) ;
#246889=CARTESIAN_POINT ( 'NONE',  ( 15.74999999999999645, 9.350000000011139178, -50.25000000000000000 ) ) ;
#247107=CARTESIAN_POINT ( 'NONE',  ( -16.87036670365549895, 9.989418819312803066, -46.02043988269794994 ) ) ;
#247227=CARTESIAN_POINT ( 'NONE',  ( -23.25000000000000355, 10.05000000001113847, -46.25000000000000711 ) ) ;
#247534=CARTESIAN_POINT ( 'NONE',  ( -16.91256925476571027, 9.985731158139330432, -46.03235751099472850 ) ) ;
#247703=ORIENTED_EDGE ( 'NONE', *, *, #187274, .T. ) ;
#247838=AXIS2_PLACEMENT_3D ( 'NONE', #103951, #203071, #162679 ) ;
#247896=EDGE_LOOP ( 'NONE', ( #124415, #28462, #84939, #159417 ) ) ;
#247898=VERTEX_POINT ( 'NONE', #895 ) ;
#248034=DIRECTION ( 'NONE',  ( -1.000000000000000000, 0.000000000000000000, 0.000000000000000000 ) ) ;
#248106=LINE ( 'NONE', #87733, #161093 ) ;
#248118=CARTESIAN_POINT ( 'NONE',  ( -16.80070461187925090, 9.950000000011103296, -54.35303617083764749 ) ) ;
#248121=DIRECTION ( 'NONE',  ( -0.000000000000000000, -0.000000000000000000, -1.000000000000000000 ) ) ;
#248438=VERTEX_POINT ( 'NONE', #210396 ) ;
#248675=AXIS2_PLACEMENT_3D ( 'NONE', #64306, #218214, #198675 ) ;
#248714=VECTOR ( 'NONE', #96670, 1000.000000000000000 ) ;
#248827=CARTESIAN_POINT ( 'NONE',  ( -18.40000000000000213, 11.47316190337364183, -57.75000000000000711 ) ) ;
#248960=CARTESIAN_POINT ( 'NONE',  ( -16.94107738177414291, 10.01423928514777373, -54.44999999999999574 ) ) ;
#249345=VERTEX_POINT ( 'NONE', #102542 ) ;
#249366=VECTOR ( 'NONE', #63084, 1000.000000000000000 ) ;
#249420=CARTESIAN_POINT ( 'NONE',  ( -16.82055514392389028, 9.950000000011140600, -54.32320192545801518 ) ) ;
#249619=CARTESIAN_POINT ( 'NONE',  ( 12.60053434924910221, 9.389534562357860992, -49.17480930438996012 ) ) ;
#250064=CARTESIAN_POINT ( 'NONE',  ( -16.93226657140833069, 9.999543822735571297, -46.07871311097362366 ) ) ;
#250118=EDGE_CURVE ( 'NONE', #97258, #215894, #14177, .T. ) ;
#250196=DIRECTION ( 'NONE',  ( -1.073024830501117725E-15, 0.000000000000000000, 1.000000000000000000 ) ) ;
#250264=EDGE_CURVE ( 'NONE', #136044, #196832, #177387, .T. ) ;
#250405=CARTESIAN_POINT ( 'NONE',  ( 18.39999999999999147, 8.822561741677553471, -42.75000000000000000 ) ) ;
#250413=( BOUNDED_CURVE ( )  B_SPLINE_CURVE ( 3, ( #227516, #69758, #46305, #205374 ),
 .UNSPECIFIED., .F., .F. ) 
 B_SPLINE_CURVE_WITH_KNOTS ( ( 4, 4 ),
 ( 0.000000000000000000, 1.570796326794896558 ),
 .UNSPECIFIED. ) 
 CURVE ( )  GEOMETRIC_REPRESENTATION_ITEM ( )  RATIONAL_B_SPLINE_CURVE ( ( 1.000000000000000000, 0.8047378541243649375, 0.8047378541243649375, 1.000000000000000000 ) ) 
 REPRESENTATION_ITEM ( '' )  );
#250424=ADVANCED_FACE ( 'NONE', ( #20875 ), #3851, .F. ) ;
#250458=DIRECTION ( 'NONE',  ( 0.5932847527679310229, -0.8049926720990042694, -6.366092712777067056E-16 ) ) ;
#250585=CARTESIAN_POINT ( 'NONE',  ( -16.97683809663752186, 9.950000000011138823, -42.75000000000000000 ) ) ;
#250724=FILL_AREA_STYLE ('',( #53816 ) ) ;
#250745=CARTESIAN_POINT ( 'NONE',  ( 15.73863059295127798, 9.351403174152808973, -50.47953043683848762 ) ) ;
#250801=ORIENTED_EDGE ( 'NONE', *, *, #49861, .F. ) ;
#250865=ORIENTED_EDGE ( 'NONE', *, *, #164644, .F. ) ;
#251015=AXIS2_PLACEMENT_3D ( 'NONE', #182320, #12357, #107566 ) ;
#251112=ORIENTED_EDGE ( 'NONE', *, *, #189487, .T. ) ;
#251311=ORIENTED_EDGE ( 'NONE', *, *, #172169, .T. ) ;
#251412=PLANE ( 'NONE',  #155895 ) ;
#251594=ORIENTED_EDGE ( 'NONE', *, *, #257151, .F. ) ;
#251723=LINE ( 'NONE', #189193, #79770 ) ;
#251915=ORIENTED_EDGE ( 'NONE', *, *, #6403, .F. ) ;
#251950=CARTESIAN_POINT ( 'NONE',  ( -18.40000000000000213, 5.650000000011139001, -46.15000000000000568 ) ) ;
#251954=ORIENTED_EDGE ( 'NONE', *, *, #219203, .T. ) ;
#252462=ORIENTED_EDGE ( 'NONE', *, *, #169743, .T. ) ;
#252736=LINE ( 'NONE', #32459, #31880 ) ;
#252740=DIRECTION ( 'NONE',  ( 1.000000000000000000, 1.186688945009010077E-16, 0.000000000000000000 ) ) ;
#252856=VECTOR ( 'NONE', #256701, 1000.000000000000000 ) ;
#252956=EDGE_CURVE ( 'NONE', #196832, #243879, #193034, .T. ) ;
#253090=( BOUNDED_CURVE ( )  B_SPLINE_CURVE ( 3, ( #2877, #84964, #246631, #104529 ),
 .UNSPECIFIED., .F., .T. ) 
 B_SPLINE_CURVE_WITH_KNOTS ( ( 4, 4 ),
 ( 5.731445031868799056, 5.983100554402348337 ),
 .UNSPECIFIED. ) 
 CURVE ( )  GEOMETRIC_REPRESENTATION_ITEM ( )  RATIONAL_B_SPLINE_CURVE ( ( 1.000000000000000000, 0.9947294176030464508, 0.9947294176030464508, 1.000000000000000000 ) ) 
 REPRESENTATION_ITEM ( '' )  );
#253155=EDGE_CURVE ( 'NONE', #126571, #151965, #58138, .T. ) ;
#253186=VERTEX_POINT ( 'NONE', #97246 ) ;
#253312=CARTESIAN_POINT ( 'NONE',  ( 12.84435279558019793, 9.410708747058235346, -51.56920840584410826 ) ) ;
#253479=DIRECTION ( 'NONE',  ( 1.000000000000000000, 0.000000000000000000, 0.000000000000000000 ) ) ;
#253557=ORIENTED_EDGE ( 'NONE', *, *, #237695, .F. ) ;
#253850=CARTESIAN_POINT ( 'NONE',  ( -16.77308656112215246, 9.950000000011137047, -46.15019319170230716 ) ) ;
#254088=CARTESIAN_POINT ( 'NONE',  ( -17.01764560440443930, 9.950000000011138823, -46.24999999921458738 ) ) ;
#254262=ADVANCED_FACE ( 'NONE', ( #131650 ), #33886, .F. ) ;
#254390=CARTESIAN_POINT ( 'NONE',  ( -16.85939681242906119, 9.905225185936458843, -54.03992195519148822 ) ) ;
#254535=CARTESIAN_POINT ( 'NONE',  ( -12.92414019175885898, 9.417632963117450018, -51.64894846573227483 ) ) ;
#254574=CARTESIAN_POINT ( 'NONE',  ( 12.93279065517211990, 9.417690691074255938, -51.64160069676457709 ) ) ;
#254764=EDGE_CURVE ( 'NONE', #100166, #27850, #189934, .T. ) ;
#254771=CARTESIAN_POINT ( 'NONE',  ( -17.11825945287482043, 9.950000000011145929, -54.35000000000000853 ) ) ;
#255168=CARTESIAN_POINT ( 'NONE',  ( -16.86445178670636835, 9.962211629127192936, -46.10922256188256085 ) ) ;
#255203=EDGE_LOOP ( 'NONE', ( #241632, #42689, #196324, #219118 ) ) ;
#255240=EDGE_LOOP ( 'NONE', ( #84143, #204762, #75512, #153420, #1780, #173539 ) ) ;
#255266=DIRECTION ( 'NONE',  ( -1.000000000000000000, 0.000000000000000000, 0.000000000000000000 ) ) ;
#255548=VECTOR ( 'NONE', #241833, 1000.000000000000000 ) ;
#255965=ORIENTED_EDGE ( 'NONE', *, *, #198863, .F. ) ;
#256099=CARTESIAN_POINT ( 'NONE',  ( -23.25000000000000355, 5.650000000011139001, -54.35000000000000142 ) ) ;
#256701=DIRECTION ( 'NONE',  ( -0.000000000000000000, 1.000000000000000000, -0.000000000000000000 ) ) ;
#256758=CARTESIAN_POINT ( 'NONE',  ( -16.94107738177414291, 10.01423928514777373, -54.44999999999999574 ) ) ;
#257014=CARTESIAN_POINT ( 'NONE',  ( -17.22767730082740556, 10.34924421247841408, -44.85757130942987914 ) ) ;
#257151=EDGE_CURVE ( 'NONE', #216000, #243879, #13920, .T. ) ;
#257180=VECTOR ( 'NONE', #40469, 1000.000000000000000 ) ;
#257184=ORIENTED_EDGE ( 'NONE', *, *, #207320, .F. ) ;
#257327=CARTESIAN_POINT ( 'NONE',  ( -16.93388492042257809, 9.988541822527059466, -54.40054512318618407 ) ) ;
#257402=CARTESIAN_POINT ( 'NONE',  ( 23.04999999999999716, 8.822561741677553471, -42.75000000000000000 ) ) ;
#257406=EDGE_CURVE ( 'NONE', #143756, #53148, #226196, .T. ) ;
#257523=CARTESIAN_POINT ( 'NONE',  ( 21.72449340488910607, 10.28395627750227703, -42.75000000000000000 ) ) ;
#257545=CARTESIAN_POINT ( 'NONE',  ( 23.04999999999999716, 8.822561741677553471, -46.15000000000001279 ) ) ;
#257575=DIRECTION ( 'NONE',  ( 1.000000000000000000, 0.000000000000000000, 0.000000000000000000 ) ) ;
#257649=CARTESIAN_POINT ( 'NONE',  ( -16.93710578446435733, 9.950000000011137047, -46.41880398379915817 ) ) ;
#257839=EDGE_CURVE ( 'NONE', #126571, #120029, #98894, .T. ) ;
#257884=UNCERTAINTY_MEASURE_WITH_UNIT (LENGTH_MEASURE( 1.000000000000000082E-05 ), #223454, 'distance_accuracy_value', 'NONE');
#258050=CARTESIAN_POINT ( 'NONE',  ( -18.44085059012131822, 11.51401249349495970, -57.74030531912154629 ) ) ;
ENDSEC;
END-ISO-10303-21;
